ISO-10303-21;
HEADER;
/* Generated by software containing ST-Developer
 * from STEP Tools, Inc. (www.steptools.com) 
 */

FILE_DESCRIPTION(
/* description */ ('Independent direct-acting normally-closed roller-plunger limit-switch
 CAD. Removable cover, insulated terminal supports, captured bus/conta
ct bridge, native Coil return spring, integral lower travel stop, reus
able instanced hardware and free roller. Manual geometric contact open
ing4mm; no snap-action/contact-force, electrical/current/voltage, envi
ronmental seal, safety-switch, wear, load or life certification. Exter
nal wiring and anchors omitted; fits and application engineering requi
red.'),
/* implementation_level */ '2;1');

FILE_NAME(
/* name */ 'Socket head cap screw M3x6.step',
/* time_stamp */ '2026-11-08T07:32:43-08:00',
/* author */ (''),
/* organization */ (''),
/* preprocessor_version */ 'ST-DEVELOPER v20.2',
/* originating_system */ 'Autodesk Translation Framework v15.17.0.0',
/* authorisation */ '');

FILE_SCHEMA (('AUTOMOTIVE_DESIGN { 1 0 10303 214 3 1 1 }'));
ENDSEC;

DATA;
#10=MECHANICAL_DESIGN_GEOMETRIC_PRESENTATION_REPRESENTATION('',(#191),#36482);
#140=CONICAL_SURFACE('',#10582,0.1,0.785398163397448);
#157=SHAPE_REPRESENTATION_RELATIONSHIP('SRR','None',#36570,#174);
#174=ADVANCED_BREP_SHAPE_REPRESENTATION('',(#208),#36480);
#191=STYLED_ITEM('',(#36659),#208);
#208=MANIFOLD_SOLID_BREP('Body1',#9782);
#231=B_SPLINE_SURFACE_WITH_KNOTS('',3,3,((#32953,#32954,#32955,#32956,#32957,
#32958,#32959,#32960,#32961,#32962,#32963,#32964,#32965,#32966,#32967,#32968,
#32969,#32970,#32971,#32972,#32973,#32974,#32975,#32976,#32977,#32978,#32979,
#32980,#32981,#32982,#32983,#32984,#32985,#32986,#32987,#32988,#32989,#32990,
#32991,#32992,#32993,#32994,#32995,#32996,#32997,#32998,#32999,#33000,#33001,
#33002,#33003,#33004,#33005,#33006,#33007,#33008,#33009,#33010,#33011,#33012,
#33013,#33014,#33015,#33016,#33017,#33018,#33019,#33020,#33021,#33022),
(#33023,#33024,#33025,#33026,#33027,#33028,#33029,#33030,#33031,#33032,
#33033,#33034,#33035,#33036,#33037,#33038,#33039,#33040,#33041,#33042,#33043,
#33044,#33045,#33046,#33047,#33048,#33049,#33050,#33051,#33052,#33053,#33054,
#33055,#33056,#33057,#33058,#33059,#33060,#33061,#33062,#33063,#33064,#33065,
#33066,#33067,#33068,#33069,#33070,#33071,#33072,#33073,#33074,#33075,#33076,
#33077,#33078,#33079,#33080,#33081,#33082,#33083,#33084,#33085,#33086,#33087,
#33088,#33089,#33090,#33091,#33092),(#33093,#33094,#33095,#33096,#33097,
#33098,#33099,#33100,#33101,#33102,#33103,#33104,#33105,#33106,#33107,#33108,
#33109,#33110,#33111,#33112,#33113,#33114,#33115,#33116,#33117,#33118,#33119,
#33120,#33121,#33122,#33123,#33124,#33125,#33126,#33127,#33128,#33129,#33130,
#33131,#33132,#33133,#33134,#33135,#33136,#33137,#33138,#33139,#33140,#33141,
#33142,#33143,#33144,#33145,#33146,#33147,#33148,#33149,#33150,#33151,#33152,
#33153,#33154,#33155,#33156,#33157,#33158,#33159,#33160,#33161,#33162),
(#33163,#33164,#33165,#33166,#33167,#33168,#33169,#33170,#33171,#33172,
#33173,#33174,#33175,#33176,#33177,#33178,#33179,#33180,#33181,#33182,#33183,
#33184,#33185,#33186,#33187,#33188,#33189,#33190,#33191,#33192,#33193,#33194,
#33195,#33196,#33197,#33198,#33199,#33200,#33201,#33202,#33203,#33204,#33205,
#33206,#33207,#33208,#33209,#33210,#33211,#33212,#33213,#33214,#33215,#33216,
#33217,#33218,#33219,#33220,#33221,#33222,#33223,#33224,#33225,#33226,#33227,
#33228,#33229,#33230,#33231,#33232)),.UNSPECIFIED.,.F.,.F.,.F.,(4,4),(4,
1,1,1,1,1,1,1,1,1,1,1,1,1,1,1,1,1,1,1,1,1,1,1,1,1,1,1,1,1,1,1,1,1,1,1,1,
1,1,1,1,1,1,1,1,1,1,1,1,1,1,1,1,1,1,1,1,1,1,1,1,1,1,1,1,1,1,4),(0.,0.0329955678841871),
(11.6159397475004,12.6141690908179,13.6123984341354,14.6106277774529,15.6088571207704,
16.6070864640879,17.6053158074054,18.6035451507229,19.6017744940404,20.600003837358,
21.5982331806755,22.596462523993,23.5946918673105,24.592921210628,25.5911505539455,
26.589379897263,27.5876092405805,28.585838583898,29.5840679272155,30.5822972705331,
31.5805266138506,32.5787559571681,33.5769853004856,34.5752146438031,35.5734439871206,
36.5716733304381,37.5699026737556,38.5681320170731,39.5663613603907,40.5645907037082,
41.5628200470257,42.5610493903432,43.5592787336607,44.5575080769782,45.5557374202957,
46.5539667636132,47.5521961069307,48.5504254502482,49.5486547935658,50.5468841368833,
51.5451134802008,52.5433428235183,53.5415721668358,54.5398015101533,55.5380308534708,
56.5362601967883,57.5344895401058,58.5327188834233,59.5309482267409,60.5291775700584,
61.5274069133759,62.5256362566934,63.5238656000109,64.5220949433284,65.5203242866459,
66.5185536299634,67.5167829732809,68.5150123165984,69.513241659916,70.5114710032335,
71.509700346551,72.5079296898685,73.506159033186,74.5043883765035,75.502617719821,
76.5008470631385,77.499076406456,78.4973057497735),.UNSPECIFIED.);
#232=B_SPLINE_SURFACE_WITH_KNOTS('',3,3,((#33322,#33323,#33324,#33325,#33326,
#33327,#33328,#33329,#33330,#33331,#33332,#33333,#33334,#33335,#33336,#33337,
#33338,#33339,#33340,#33341,#33342,#33343,#33344,#33345,#33346,#33347,#33348,
#33349,#33350,#33351,#33352,#33353,#33354,#33355,#33356,#33357,#33358,#33359,
#33360,#33361,#33362,#33363,#33364,#33365,#33366,#33367,#33368,#33369,#33370,
#33371,#33372,#33373,#33374,#33375,#33376,#33377,#33378,#33379,#33380,#33381,
#33382,#33383,#33384,#33385,#33386,#33387,#33388,#33389,#33390,#33391,#33392,
#33393),(#33394,#33395,#33396,#33397,#33398,#33399,#33400,#33401,#33402,
#33403,#33404,#33405,#33406,#33407,#33408,#33409,#33410,#33411,#33412,#33413,
#33414,#33415,#33416,#33417,#33418,#33419,#33420,#33421,#33422,#33423,#33424,
#33425,#33426,#33427,#33428,#33429,#33430,#33431,#33432,#33433,#33434,#33435,
#33436,#33437,#33438,#33439,#33440,#33441,#33442,#33443,#33444,#33445,#33446,
#33447,#33448,#33449,#33450,#33451,#33452,#33453,#33454,#33455,#33456,#33457,
#33458,#33459,#33460,#33461,#33462,#33463,#33464,#33465),(#33466,#33467,
#33468,#33469,#33470,#33471,#33472,#33473,#33474,#33475,#33476,#33477,#33478,
#33479,#33480,#33481,#33482,#33483,#33484,#33485,#33486,#33487,#33488,#33489,
#33490,#33491,#33492,#33493,#33494,#33495,#33496,#33497,#33498,#33499,#33500,
#33501,#33502,#33503,#33504,#33505,#33506,#33507,#33508,#33509,#33510,#33511,
#33512,#33513,#33514,#33515,#33516,#33517,#33518,#33519,#33520,#33521,#33522,
#33523,#33524,#33525,#33526,#33527,#33528,#33529,#33530,#33531,#33532,#33533,
#33534,#33535,#33536,#33537),(#33538,#33539,#33540,#33541,#33542,#33543,
#33544,#33545,#33546,#33547,#33548,#33549,#33550,#33551,#33552,#33553,#33554,
#33555,#33556,#33557,#33558,#33559,#33560,#33561,#33562,#33563,#33564,#33565,
#33566,#33567,#33568,#33569,#33570,#33571,#33572,#33573,#33574,#33575,#33576,
#33577,#33578,#33579,#33580,#33581,#33582,#33583,#33584,#33585,#33586,#33587,
#33588,#33589,#33590,#33591,#33592,#33593,#33594,#33595,#33596,#33597,#33598,
#33599,#33600,#33601,#33602,#33603,#33604,#33605,#33606,#33607,#33608,#33609)),
 .UNSPECIFIED.,.F.,.F.,.F.,(4,4),(4,1,1,1,1,1,1,1,1,1,1,1,1,1,1,1,1,1,1,
1,1,1,1,1,1,1,1,1,1,1,1,1,1,1,1,1,1,1,1,1,1,1,1,1,1,1,1,1,1,1,1,1,1,1,1,
1,1,1,1,1,1,1,1,1,1,1,1,1,1,4),(0.,0.0329955678841871),(8.30203615430834,
9.30137729453432,10.3007184347603,11.3000595749863,12.2994007152123,13.2987418554383,
14.2980829956642,15.2974241358902,16.2967652761162,17.2961064163422,18.2954475565682,
19.2947886967942,20.2941298370201,21.2934709772461,22.2928121174721,23.2921532576981,
24.2914943979241,25.2908355381501,26.290176678376,27.289517818602,28.288858958828,
29.288200099054,30.28754123928,31.286882379506,32.2862235197319,33.2855646599579,
34.2849058001839,35.2842469404099,36.2835880806359,37.2829292208619,38.2822703610879,
39.2816115013138,40.2809526415398,41.2802937817658,42.2796349219918,43.2789760622178,
44.2783172024438,45.2776583426697,46.2769994828957,47.2763406231217,48.2756817633477,
49.2750229035737,50.2743640437997,51.2737051840256,52.2730463242516,53.2723874644776,
54.2717286047036,55.2710697449296,56.2704108851556,57.2697520253815,58.2690931656075,
59.2684343058335,60.2677754460595,61.2671165862855,62.2664577265115,63.2657988667374,
64.2651400069634,65.2644811471894,66.2638222874154,67.2631634276414,68.2625045678674,
69.2618457080933,70.2611868483193,71.2605279885453,72.2598691287713,73.2592102689973,
74.2585514092233,75.2578925494492,76.2572336896752,77.2565748299012),
 .UNSPECIFIED.);
#298=FACE_BOUND('',#1523,.T.);
#299=FACE_BOUND('',#1526,.T.);
#419=PLANE('',#10588);
#420=PLANE('',#10589);
#421=PLANE('',#10590);
#422=PLANE('',#10591);
#423=PLANE('',#10592);
#424=PLANE('',#10593);
#425=PLANE('',#10594);
#426=PLANE('',#10595);
#427=PLANE('',#10599);
#428=PLANE('',#10600);
#889=FACE_OUTER_BOUND('',#1490,.T.);
#890=FACE_OUTER_BOUND('',#1491,.T.);
#891=FACE_OUTER_BOUND('',#1492,.T.);
#892=FACE_OUTER_BOUND('',#1493,.T.);
#893=FACE_OUTER_BOUND('',#1494,.T.);
#894=FACE_OUTER_BOUND('',#1495,.T.);
#895=FACE_OUTER_BOUND('',#1496,.T.);
#896=FACE_OUTER_BOUND('',#1497,.T.);
#897=FACE_OUTER_BOUND('',#1498,.T.);
#898=FACE_OUTER_BOUND('',#1499,.T.);
#899=FACE_OUTER_BOUND('',#1500,.T.);
#900=FACE_OUTER_BOUND('',#1501,.T.);
#901=FACE_OUTER_BOUND('',#1502,.T.);
#902=FACE_OUTER_BOUND('',#1503,.T.);
#903=FACE_OUTER_BOUND('',#1504,.T.);
#904=FACE_OUTER_BOUND('',#1505,.T.);
#905=FACE_OUTER_BOUND('',#1506,.T.);
#906=FACE_OUTER_BOUND('',#1507,.T.);
#907=FACE_OUTER_BOUND('',#1508,.T.);
#908=FACE_OUTER_BOUND('',#1509,.T.);
#909=FACE_OUTER_BOUND('',#1510,.T.);
#910=FACE_OUTER_BOUND('',#1511,.T.);
#911=FACE_OUTER_BOUND('',#1512,.T.);
#912=FACE_OUTER_BOUND('',#1513,.T.);
#913=FACE_OUTER_BOUND('',#1514,.T.);
#914=FACE_OUTER_BOUND('',#1515,.T.);
#915=FACE_OUTER_BOUND('',#1516,.T.);
#916=FACE_OUTER_BOUND('',#1517,.T.);
#917=FACE_OUTER_BOUND('',#1518,.T.);
#918=FACE_OUTER_BOUND('',#1519,.T.);
#919=FACE_OUTER_BOUND('',#1520,.T.);
#920=FACE_OUTER_BOUND('',#1521,.T.);
#921=FACE_OUTER_BOUND('',#1522,.T.);
#922=FACE_OUTER_BOUND('',#1524,.T.);
#923=FACE_OUTER_BOUND('',#1525,.T.);
#924=FACE_OUTER_BOUND('',#1527,.T.);
#1490=EDGE_LOOP('',(#8380,#8381,#8382,#8383));
#1491=EDGE_LOOP('',(#8384,#8385,#8386,#8387));
#1492=EDGE_LOOP('',(#8388,#8389,#8390,#8391));
#1493=EDGE_LOOP('',(#8392,#8393,#8394,#8395));
#1494=EDGE_LOOP('',(#8396,#8397,#8398,#8399));
#1495=EDGE_LOOP('',(#8400,#8401,#8402,#8403));
#1496=EDGE_LOOP('',(#8404,#8405,#8406,#8407));
#1497=EDGE_LOOP('',(#8408,#8409,#8410,#8411));
#1498=EDGE_LOOP('',(#8412,#8413,#8414,#8415));
#1499=EDGE_LOOP('',(#8416,#8417,#8418,#8419));
#1500=EDGE_LOOP('',(#8420,#8421,#8422,#8423));
#1501=EDGE_LOOP('',(#8424,#8425,#8426,#8427));
#1502=EDGE_LOOP('',(#8428,#8429,#8430,#8431));
#1503=EDGE_LOOP('',(#8432,#8433,#8434,#8435));
#1504=EDGE_LOOP('',(#8436,#8437,#8438,#8439));
#1505=EDGE_LOOP('',(#8440,#8441,#8442,#8443));
#1506=EDGE_LOOP('',(#8444,#8445,#8446,#8447));
#1507=EDGE_LOOP('',(#8448,#8449,#8450,#8451));
#1508=EDGE_LOOP('',(#8452,#8453,#8454,#8455));
#1509=EDGE_LOOP('',(#8456,#8457,#8458,#8459));
#1510=EDGE_LOOP('',(#8460,#8461,#8462,#8463,#8464,#8465,#8466,#8467));
#1511=EDGE_LOOP('',(#8468,#8469,#8470,#8471,#8472,#8473,#8474,#8475,#8476,
#8477,#8478,#8479,#8480,#8481,#8482,#8483,#8484,#8485,#8486,#8487,#8488,
#8489,#8490,#8491));
#1512=EDGE_LOOP('',(#8492,#8493,#8494,#8495));
#1513=EDGE_LOOP('',(#8496,#8497,#8498,#8499,#8500,#8501,#8502,#8503,#8504,
#8505,#8506,#8507,#8508,#8509,#8510,#8511,#8512,#8513,#8514,#8515,#8516,
#8517,#8518,#8519,#8520));
#1514=EDGE_LOOP('',(#8521,#8522,#8523,#8524));
#1515=EDGE_LOOP('',(#8525,#8526,#8527,#8528));
#1516=EDGE_LOOP('',(#8529,#8530,#8531,#8532));
#1517=EDGE_LOOP('',(#8533,#8534,#8535,#8536));
#1518=EDGE_LOOP('',(#8537,#8538,#8539,#8540));
#1519=EDGE_LOOP('',(#8541,#8542,#8543,#8544));
#1520=EDGE_LOOP('',(#8545,#8546,#8547,#8548));
#1521=EDGE_LOOP('',(#8549,#8550,#8551,#8552,#8553,#8554));
#1522=EDGE_LOOP('',(#8555));
#1523=EDGE_LOOP('',(#8556,#8557,#8558,#8559));
#1524=EDGE_LOOP('',(#8560,#8561,#8562,#8563));
#1525=EDGE_LOOP('',(#8564));
#1526=EDGE_LOOP('',(#8565,#8566,#8567,#8568,#8569,#8570));
#1527=EDGE_LOOP('',(#8571));
#1724=CIRCLE('',#10561,0.14635);
#1725=CIRCLE('',#10572,0.117775);
#1726=CIRCLE('',#10583,0.14635);
#1727=CIRCLE('',#10584,0.05);
#1728=CIRCLE('',#10586,0.117775);
#1729=CIRCLE('',#10596,0.3);
#1730=CIRCLE('',#10598,0.3);
#2315=B_SPLINE_CURVE_WITH_KNOTS('',3,(#32059,#32060,#32061,#32062,#32063,
#32064,#32065,#32066,#32067,#32068),.UNSPECIFIED.,.F.,.F.,(4,3,3,4),(-4.09202352044854,
-3.99291737327004,-2.99468802995253,-2.07317267331973),.UNSPECIFIED.);
#2316=B_SPLINE_CURVE_WITH_KNOTS('',3,(#32071,#32072,#32073,#32074,#32075,
#32076,#32077),.UNSPECIFIED.,.F.,.F.,(4,3,4),(0.,0.999341140225982,1.12274180646093),
 .UNSPECIFIED.);
#2317=B_SPLINE_CURVE_WITH_KNOTS('',3,(#32082,#32083,#32084,#32085,#32086,
#32087,#32088,#32089,#32090,#32091,#32092,#32093,#32094,#32095,#32096,#32097,
#32098,#32099,#32100,#32101,#32102,#32103),.UNSPECIFIED.,.F.,.F.,(4,3,3,
3,3,3,3,4),(-10.3752088276281,-9.9822934331751,-8.98406408985759,-7.98583474654008,
-6.98760540322257,-5.98937605990506,-4.99114671658755,-4.09202352044854),
 .UNSPECIFIED.);
#2318=B_SPLINE_CURVE_WITH_KNOTS('',3,(#32104,#32105,#32106,#32107,#32108,
#32109,#32110,#32111,#32112,#32113,#32114,#32115,#32116,#32117,#32118,#32119,
#32120,#32121,#32122,#32123,#32124,#32125),.UNSPECIFIED.,.F.,.F.,(4,3,3,
3,3,3,3,4),(1.12274180646093,1.99868228045197,2.99802342067795,3.99736456090394,
4.99670570112992,5.99604684135591,6.99538798158189,7.40592711364052),
 .UNSPECIFIED.);
#2319=B_SPLINE_CURVE_WITH_KNOTS('',3,(#32130,#32131,#32132,#32133,#32134,
#32135,#32136,#32137,#32138,#32139,#32140,#32141,#32142,#32143,#32144,#32145,
#32146,#32147,#32148,#32149,#32150,#32151),.UNSPECIFIED.,.F.,.F.,(4,3,3,
3,3,3,3,4),(-16.6583941348077,-15.9716694930802,-14.9734401497627,-13.9752108064451,
-12.9769814631276,-11.9787521198101,-10.9805227764926,-10.3752088276281),
 .UNSPECIFIED.);
#2320=B_SPLINE_CURVE_WITH_KNOTS('',3,(#32152,#32153,#32154,#32155,#32156,
#32157,#32158,#32159,#32160,#32161,#32162,#32163,#32164,#32165,#32166,#32167,
#32168,#32169,#32170,#32171,#32172,#32173),.UNSPECIFIED.,.F.,.F.,(4,3,3,
3,3,3,3,4),(7.40592711364052,7.99472912180787,8.99407026203386,9.99341140225984,
10.9927525424858,11.9920936827118,12.9914348229378,13.6891124208201),
 .UNSPECIFIED.);
#2321=B_SPLINE_CURVE_WITH_KNOTS('',3,(#32178,#32179,#32180,#32181,#32182,
#32183,#32184,#32185,#32186,#32187,#32188,#32189,#32190,#32191,#32192,#32193,
#32194,#32195,#32196,#32197,#32198,#32199),.UNSPECIFIED.,.F.,.F.,(4,3,3,
3,3,3,3,4),(-22.9415794419873,-21.9610455529852,-20.9628162096677,-19.9645868663502,
-18.9663575230327,-17.9681281797152,-16.9698988363977,-16.6583941348077),
 .UNSPECIFIED.);
#2322=B_SPLINE_CURVE_WITH_KNOTS('',3,(#32200,#32201,#32202,#32203,#32204,
#32205,#32206,#32207,#32208,#32209,#32210,#32211,#32212,#32213,#32214,#32215,
#32216,#32217,#32218,#32219,#32220,#32221),.UNSPECIFIED.,.F.,.F.,(4,3,3,
3,3,3,3,4),(13.6891124208201,13.9907759631638,14.9901171033898,15.9894582436157,
16.9887993838417,17.9881405240677,18.9874816642937,19.9722977279997),
 .UNSPECIFIED.);
#2323=B_SPLINE_CURVE_WITH_KNOTS('',3,(#32226,#32227,#32228,#32229,#32230,
#32231,#32232,#32233,#32234,#32235,#32236,#32237,#32238,#32239,#32240,#32241,
#32242,#32243,#32244,#32245,#32246,#32247,#32248,#32249,#32250),
 .UNSPECIFIED.,.F.,.F.,(4,3,3,3,3,3,3,3,4),(-29.2247647491669,-28.9486509562078,
-27.9504216128903,-26.9521922695728,-25.9539629262553,-24.9557335829378,
-23.9575042396202,-22.9592748963027,-22.9415794419873),.UNSPECIFIED.);
#2324=B_SPLINE_CURVE_WITH_KNOTS('',3,(#32251,#32252,#32253,#32254,#32255,
#32256,#32257,#32258,#32259,#32260,#32261,#32262,#32263,#32264,#32265,#32266,
#32267,#32268,#32269,#32270,#32271,#32272,#32273,#32274,#32275),
 .UNSPECIFIED.,.F.,.F.,(4,3,3,3,3,3,3,3,4),(19.9722977279997,19.9868228045197,
20.9861639447457,21.9855050849716,22.9848462251976,23.9841873654236,24.9835285056496,
25.9828696458756,26.2554830351793),.UNSPECIFIED.);
#2325=B_SPLINE_CURVE_WITH_KNOTS('',3,(#32280,#32281,#32282,#32283,#32284,
#32285,#32286,#32287,#32288,#32289,#32290,#32291,#32292,#32293,#32294,#32295,
#32296,#32297,#32298,#32299,#32300,#32301),.UNSPECIFIED.,.F.,.F.,(4,3,3,
3,3,3,3,4),(-35.5079500563465,-34.9380270161129,-33.9397976727954,-32.9415683294778,
-31.9433389861603,-30.9451096428428,-29.9468802995253,-29.2247647491669),
 .UNSPECIFIED.);
#2326=B_SPLINE_CURVE_WITH_KNOTS('',3,(#32302,#32303,#32304,#32305,#32306,
#32307,#32308,#32309,#32310,#32311,#32312,#32313,#32314,#32315,#32316,#32317,
#32318,#32319,#32320,#32321,#32322,#32323),.UNSPECIFIED.,.F.,.F.,(4,3,3,
3,3,3,3,4),(26.2554830351793,26.9822107861016,27.9815519263275,28.9808930665535,
29.9802342067795,30.9795753470055,31.9789164872315,32.5386683423589),
 .UNSPECIFIED.);
#2327=B_SPLINE_CURVE_WITH_KNOTS('',3,(#32328,#32329,#32330,#32331,#32332,
#32333,#32334,#32335,#32336,#32337,#32338,#32339,#32340,#32341,#32342,#32343,
#32344,#32345,#32346,#32347,#32348,#32349),.UNSPECIFIED.,.F.,.F.,(4,3,3,
3,3,3,3,4),(-41.7911353635261,-40.9274030760179,-39.9291737327004,-38.9309443893829,
-37.9327150460654,-36.9344857027479,-35.9362563594304,-35.5079500563465),
 .UNSPECIFIED.);
#2328=B_SPLINE_CURVE_WITH_KNOTS('',3,(#32350,#32351,#32352,#32353,#32354,
#32355,#32356,#32357,#32358,#32359,#32360,#32361,#32362,#32363,#32364,#32365,
#32366,#32367,#32368,#32369,#32370,#32371),.UNSPECIFIED.,.F.,.F.,(4,3,3,
3,3,3,3,4),(32.5386683423589,32.9782576274575,33.9775987676834,34.9769399079094,
35.9762810481354,36.9756221883614,37.9749633285874,38.8218536495385),
 .UNSPECIFIED.);
#2329=B_SPLINE_CURVE_WITH_KNOTS('',3,(#32376,#32377,#32378,#32379,#32380,
#32381,#32382,#32383,#32384,#32385,#32386,#32387,#32388,#32389,#32390,#32391,
#32392,#32393,#32394,#32395,#32396,#32397,#32398,#32399,#32400),
 .UNSPECIFIED.,.F.,.F.,(4,3,3,3,3,3,3,3,4),(-48.0743206707057,-47.9150084792405,
-46.916779135923,-45.9185497926055,-44.920320449288,-43.9220911059705,-42.9238617626529,
-41.9256324193354,-41.7911353635261),.UNSPECIFIED.);
#2330=B_SPLINE_CURVE_WITH_KNOTS('',3,(#32401,#32402,#32403,#32404,#32405,
#32406,#32407,#32408,#32409,#32410,#32411,#32412,#32413,#32414,#32415,#32416,
#32417,#32418,#32419,#32420,#32421,#32422,#32423,#32424,#32425),
 .UNSPECIFIED.,.F.,.F.,(4,3,3,3,3,3,3,3,4),(38.8218536495385,38.9743044688134,
39.9736456090394,40.9729867492653,41.9723278894913,42.9716690297173,43.9710101699433,
44.9703513101693,45.105038956718),.UNSPECIFIED.);
#2331=B_SPLINE_CURVE_WITH_KNOTS('',3,(#32430,#32431,#32432,#32433,#32434,
#32435,#32436,#32437,#32438,#32439,#32440,#32441,#32442,#32443,#32444,#32445,
#32446,#32447,#32448,#32449,#32450,#32451),.UNSPECIFIED.,.F.,.F.,(4,3,3,
3,3,3,3,4),(-54.3575059778853,-53.9043845391456,-52.906155195828,-51.9079258525105,
-50.909696509193,-49.9114671658755,-48.913237822558,-48.0743206707057),
 .UNSPECIFIED.);
#2332=B_SPLINE_CURVE_WITH_KNOTS('',3,(#32452,#32453,#32454,#32455,#32456,
#32457,#32458,#32459,#32460,#32461,#32462,#32463,#32464,#32465,#32466,#32467,
#32468,#32469,#32470,#32471,#32472,#32473),.UNSPECIFIED.,.F.,.F.,(4,3,3,
3,3,3,3,4),(45.105038956718,45.9696924503953,46.9690335906212,47.9683747308472,
48.9677158710732,49.9670570112992,50.9663981515252,51.3882242638976),
 .UNSPECIFIED.);
#2333=B_SPLINE_CURVE_WITH_KNOTS('',3,(#32478,#32479,#32480,#32481,#32482,
#32483,#32484,#32485,#32486,#32487,#32488,#32489,#32490,#32491,#32492,#32493,
#32494,#32495,#32496,#32497,#32498,#32499),.UNSPECIFIED.,.F.,.F.,(4,3,3,
3,3,3,3,4),(-60.6406912850648,-59.8937605990506,-58.8955312557331,-57.8973019124156,
-56.8990725690981,-55.9008432257806,-54.9026138824631,-54.3575059778853),
 .UNSPECIFIED.);
#2334=B_SPLINE_CURVE_WITH_KNOTS('',3,(#32500,#32501,#32502,#32503,#32504,
#32505,#32506,#32507,#32508,#32509,#32510,#32511,#32512,#32513,#32514,#32515,
#32516,#32517,#32518,#32519,#32520,#32521),.UNSPECIFIED.,.F.,.F.,(4,3,3,
3,3,3,3,4),(51.3882242638976,51.9657392917511,52.9650804319771,53.9644215722031,
54.9637627124291,55.9631038526551,56.9624449928811,57.6714095710772),
 .UNSPECIFIED.);
#2335=B_SPLINE_CURVE_WITH_KNOTS('',3,(#32527,#32528,#32529,#32530,#32531,
#32532,#32533,#32534,#32535,#32536),.UNSPECIFIED.,.F.,.F.,(4,1,1,1,1,1,
1,4),(72.2566310325653,72.5079296898685,73.506159033186,74.5043883765035,
75.502617719821,76.5008470631385,77.499076406456,78.4973057497735),
 .UNSPECIFIED.);
#2336=B_SPLINE_CURVE_WITH_KNOTS('',3,(#32539,#32540,#32541,#32542,#32543,
#32544,#32545,#32546,#32547),.UNSPECIFIED.,.F.,.F.,(4,1,1,1,1,1,4),(72.2566310325652,
72.2598691287713,73.2592102689973,74.2585514092233,75.2578925494492,76.2572336896752,
77.2565748299012),.UNSPECIFIED.);
#2337=B_SPLINE_CURVE_WITH_KNOTS('',3,(#32552,#32553,#32554,#32555,#32556,
#32557,#32558,#32559,#32560,#32561),.UNSPECIFIED.,.F.,.F.,(4,1,1,1,1,1,
1,4),(65.9734457253856,66.5185536299634,67.5167829732809,68.5150123165984,
69.513241659916,70.5114710032335,71.509700346551,72.2566310325653),
 .UNSPECIFIED.);
#2338=B_SPLINE_CURVE_WITH_KNOTS('',3,(#32562,#32563,#32564,#32565,#32566,
#32567,#32568,#32569,#32570,#32571),.UNSPECIFIED.,.F.,.F.,(4,1,1,1,1,1,
1,4),(65.9734457253856,66.2638222874154,67.2631634276414,68.2625045678674,
69.2618457080933,70.2611868483193,71.2605279885453,72.2566310325652),
 .UNSPECIFIED.);
#2339=B_SPLINE_CURVE_WITH_KNOTS('',3,(#32576,#32577,#32578,#32579,#32580,
#32581,#32582,#32583,#32584,#32585),.UNSPECIFIED.,.F.,.F.,(4,1,1,1,1,1,
1,4),(59.6902604182061,60.5291775700584,61.5274069133759,62.5256362566934,
63.5238656000109,64.5220949433284,65.5203242866459,65.9734457253856),
 .UNSPECIFIED.);
#2340=B_SPLINE_CURVE_WITH_KNOTS('',3,(#32586,#32587,#32588,#32589,#32590,
#32591,#32592,#32593,#32594,#32595),.UNSPECIFIED.,.F.,.F.,(4,1,1,1,1,1,
1,4),(59.6902604182061,60.2677754460595,61.2671165862855,62.2664577265115,
63.2657988667374,64.2651400069634,65.2644811471894,65.9734457253856),
 .UNSPECIFIED.);
#2341=B_SPLINE_CURVE_WITH_KNOTS('',3,(#32600,#32601,#32602,#32603,#32604,
#32605,#32606,#32607,#32608,#32609,#32610),.UNSPECIFIED.,.F.,.F.,(4,1,1,
1,1,1,1,1,4),(53.4070751110265,53.5415721668358,54.5398015101533,55.5380308534708,
56.5362601967883,57.5344895401058,58.5327188834233,59.5309482267409,59.6902604182061),
 .UNSPECIFIED.);
#2342=B_SPLINE_CURVE_WITH_KNOTS('',3,(#32611,#32612,#32613,#32614,#32615,
#32616,#32617,#32618,#32619,#32620),.UNSPECIFIED.,.F.,.F.,(4,1,1,1,1,1,
1,4),(53.4070751110265,54.2717286047036,55.2710697449296,56.2704108851556,
57.2697520253815,58.2690931656075,59.2684343058335,59.6902604182061),
 .UNSPECIFIED.);
#2343=B_SPLINE_CURVE_WITH_KNOTS('',3,(#32625,#32626,#32627,#32628,#32629,
#32630,#32631,#32632,#32633,#32634),.UNSPECIFIED.,.F.,.F.,(4,1,1,1,1,1,
1,4),(47.1238898038469,47.5521961069307,48.5504254502482,49.5486547935658,
50.5468841368833,51.5451134802008,52.5433428235183,53.4070751110265),
 .UNSPECIFIED.);
#2344=B_SPLINE_CURVE_WITH_KNOTS('',3,(#32635,#32636,#32637,#32638,#32639,
#32640,#32641,#32642,#32643,#32644,#32645),.UNSPECIFIED.,.F.,.F.,(4,1,1,
1,1,1,1,1,4),(47.1238898038469,47.2763406231217,48.2756817633477,49.2750229035737,
50.2743640437997,51.2737051840256,52.2730463242516,53.2723874644776,53.4070751110265),
 .UNSPECIFIED.);
#2345=B_SPLINE_CURVE_WITH_KNOTS('',3,(#32650,#32651,#32652,#32653,#32654,
#32655,#32656,#32657,#32658,#32659),.UNSPECIFIED.,.F.,.F.,(4,1,1,1,1,1,
1,4),(40.8407044966673,41.5628200470257,42.5610493903432,43.5592787336607,
44.5575080769782,45.5557374202957,46.5539667636132,47.1238898038469),
 .UNSPECIFIED.);
#2346=B_SPLINE_CURVE_WITH_KNOTS('',3,(#32660,#32661,#32662,#32663,#32664,
#32665,#32666,#32667,#32668,#32669),.UNSPECIFIED.,.F.,.F.,(4,1,1,1,1,1,
1,4),(40.8407044966673,41.2802937817658,42.2796349219918,43.2789760622178,
44.2783172024438,45.2776583426697,46.2769994828957,47.1238898038469),
 .UNSPECIFIED.);
#2347=B_SPLINE_CURVE_WITH_KNOTS('',3,(#32674,#32675,#32676,#32677,#32678,
#32679,#32680,#32681,#32682,#32683,#32684),.UNSPECIFIED.,.F.,.F.,(4,1,1,
1,1,1,1,1,4),(34.5575191894877,34.5752146438031,35.5734439871206,36.5716733304381,
37.5699026737556,38.5681320170731,39.5663613603907,40.5645907037082,40.8407044966673),
 .UNSPECIFIED.);
#2348=B_SPLINE_CURVE_WITH_KNOTS('',3,(#32685,#32686,#32687,#32688,#32689,
#32690,#32691,#32692,#32693,#32694),.UNSPECIFIED.,.F.,.F.,(4,1,1,1,1,1,
1,4),(34.5575191894877,35.2842469404099,36.2835880806359,37.2829292208619,
38.2822703610879,39.2816115013138,40.2809526415398,40.8407044966673),
 .UNSPECIFIED.);
#2349=B_SPLINE_CURVE_WITH_KNOTS('',3,(#32699,#32700,#32701,#32702,#32703,
#32704,#32705,#32706,#32707,#32708),.UNSPECIFIED.,.F.,.F.,(4,1,1,1,1,1,
1,4),(28.2743338823081,28.585838583898,29.5840679272155,30.5822972705331,
31.5805266138506,32.5787559571681,33.5769853004856,34.5575191894877),
 .UNSPECIFIED.);
#2350=B_SPLINE_CURVE_WITH_KNOTS('',3,(#32709,#32710,#32711,#32712,#32713,
#32714,#32715,#32716,#32717,#32718,#32719),.UNSPECIFIED.,.F.,.F.,(4,1,1,
1,1,1,1,1,4),(28.2743338823081,28.288858958828,29.288200099054,30.28754123928,
31.286882379506,32.2862235197319,33.2855646599579,34.2849058001839,34.5575191894877),
 .UNSPECIFIED.);
#2351=B_SPLINE_CURVE_WITH_KNOTS('',3,(#32724,#32725,#32726,#32727,#32728,
#32729,#32730,#32731,#32732,#32733),.UNSPECIFIED.,.F.,.F.,(4,1,1,1,1,1,
1,4),(21.9911485751285,22.596462523993,23.5946918673105,24.592921210628,
25.5911505539455,26.589379897263,27.5876092405805,28.2743338823081),
 .UNSPECIFIED.);
#2352=B_SPLINE_CURVE_WITH_KNOTS('',3,(#32734,#32735,#32736,#32737,#32738,
#32739,#32740,#32741,#32742,#32743),.UNSPECIFIED.,.F.,.F.,(4,1,1,1,1,1,
1,4),(21.9911485751285,22.2928121174721,23.2921532576981,24.2914943979241,
25.2908355381501,26.290176678376,27.289517818602,28.2743338823081),
 .UNSPECIFIED.);
#2353=B_SPLINE_CURVE_WITH_KNOTS('',3,(#32748,#32749,#32750,#32751,#32752,
#32753,#32754,#32755,#32756,#32757),.UNSPECIFIED.,.F.,.F.,(4,1,1,1,1,1,
1,4),(15.7079632679489,16.6070864640879,17.6053158074054,18.6035451507229,
19.6017744940404,20.600003837358,21.5982331806755,21.9911485751285),
 .UNSPECIFIED.);
#2354=B_SPLINE_CURVE_WITH_KNOTS('',3,(#32758,#32759,#32760,#32761,#32762,
#32763,#32764,#32765,#32766,#32767),.UNSPECIFIED.,.F.,.F.,(4,1,1,1,1,1,
1,4),(15.7079632679489,16.2967652761162,17.2961064163422,18.2954475565682,
19.2947886967942,20.2941298370201,21.2934709772461,21.9911485751285),
 .UNSPECIFIED.);
#2355=B_SPLINE_CURVE_WITH_KNOTS('',3,(#32770,#32771,#32772,#32773,#32774,
#32775,#32776,#32777,#32778,#32779,#32780,#32781,#32782,#32783,#32784,#32785,
#32786,#32787,#32788,#32789,#32790,#32791,#32792,#32793,#32794,#32795,#32796,
#32797,#32798,#32799,#32800,#32801,#32802,#32803,#32804,#32805,#32806,#32807,
#32808,#32809,#32810,#32811,#32812,#32813,#32814,#32815,#32816,#32817,#32818,
#32819,#32820,#32821,#32822,#32823,#32824,#32825,#32826,#32827,#32828,#32829,
#32830,#32831,#32832,#32833,#32834,#32835,#32836,#32837,#32838,#32839,#32840,
#32841,#32842,#32843,#32844,#32845,#32846,#32847,#32848,#32849,#32850,#32851,
#32852,#32853,#32854,#32855,#32856,#32857,#32858,#32859,#32860,#32861,#32862,
#32863,#32864,#32865,#32866,#32867,#32868,#32869,#32870,#32871,#32872,#32873,
#32874,#32875,#32876,#32877,#32878,#32879,#32880,#32881,#32882,#32883,#32884,
#32885,#32886,#32887,#32888,#32889,#32890,#32891,#32892,#32893),
 .UNSPECIFIED.,.F.,.F.,(4,3,3,3,3,3,3,3,3,3,3,3,3,3,3,3,3,3,3,3,3,3,3,3,
3,3,3,3,3,3,3,3,3,3,3,3,3,3,3,3,3,4),(-0.753008129282183,-0.726412785409006,
-0.715916399573649,-0.694852053413067,-0.683242780289961,-0.673766450589417,
-0.652778815266657,-0.639500919906121,-0.631791179943898,-0.604637195598433,
-0.591408327349303,-0.58243092328052,-0.553935160168246,-0.540392555827386,
-0.528208940192808,-0.505508318677634,-0.491429191967348,-0.477982436820105,
-0.452062180399923,-0.438863938010204,-0.427153921531904,-0.400727666335641,
-0.382198730280871,-0.374301411139377,-0.345303428221882,-0.331998698266984,
-0.322788462765202,-0.292662279142726,-0.279737557595205,-0.270213961274558,
-0.2400599353808,-0.238094602813322,-0.224912522130576,-0.21640841250359,
-0.186556730675161,-0.170795284707343,-0.161336087437576,-0.129168886313724,
-0.116523493465494,-0.106577361616136,-0.097001685189873,-0.096536015547866),
 .UNSPECIFIED.);
#2356=B_SPLINE_CURVE_WITH_KNOTS('',3,(#32895,#32896,#32897,#32898,#32899,
#32900,#32901,#32902,#32903,#32904,#32905,#32906,#32907,#32908,#32909,#32910,
#32911,#32912,#32913,#32914,#32915,#32916,#32917,#32918,#32919,#32920,#32921,
#32922,#32923,#32924,#32925,#32926,#32927,#32928,#32929,#32930,#32931),
 .UNSPECIFIED.,.F.,.F.,(4,3,3,3,3,3,3,3,3,3,3,3,4),(-0.204609524178328,
-0.17392271218969,-0.152224313672341,-0.142809800777549,-0.129914959151416,
-0.113620867578377,-0.100585910230378,-0.0924114342381335,-0.0693085756786001,
-0.0545304238088379,-0.0417479715798885,-0.0152833907299223,0.),
 .UNSPECIFIED.);
#2357=B_SPLINE_CURVE_WITH_KNOTS('',3,(#32934,#32935,#32936,#32937,#32938,
#32939,#32940,#32941,#32942,#32943,#32944,#32945,#32946,#32947,#32948,#32949),
 .UNSPECIFIED.,.F.,.F.,(4,3,3,3,3,4),(-0.096536015547866,-0.0724020116608995,
-0.0590251911255789,-0.0503900123732228,-0.0186970194324831,0.),
 .UNSPECIFIED.);
#2358=B_SPLINE_CURVE_WITH_KNOTS('',3,(#33234,#33235,#33236,#33237,#33238,
#33239,#33240,#33241),.UNSPECIFIED.,.F.,.F.,(4,1,1,1,1,4),(11.6159397475004,
12.6141690908179,13.6123984341354,14.6106277774529,15.6088571207704,15.7079632679489),
 .UNSPECIFIED.);
#2359=B_SPLINE_CURVE_WITH_KNOTS('',3,(#33242,#33243,#33244,#33245,#33246,
#33247,#33248,#33249,#33250,#33251,#33252,#33253,#33254,#33255,#33256,#33257,
#33258,#33259,#33260,#33261,#33262,#33263,#33264,#33265,#33266,#33267,#33268,
#33269,#33270,#33271,#33272,#33273,#33274,#33275,#33276,#33277,#33278,#33279,
#33280,#33281,#33282,#33283,#33284,#33285,#33286,#33287,#33288,#33289,#33290),
 .UNSPECIFIED.,.F.,.F.,(4,3,3,3,3,3,3,3,3,3,3,3,3,3,3,3,4),(-0.275362278356883,
-0.264159546247523,-0.242523917618953,-0.228489201611509,-0.209076761803474,
-0.198077656999141,-0.168436231356347,-0.151777330299101,-0.139830254922987,
-0.12544363295055,-0.101855794992709,-0.0891849033129337,-0.0668886774847003,
-0.0515641266869526,-0.0405229119346731,-0.0142790183076863,0.),
 .UNSPECIFIED.);
#2360=B_SPLINE_CURVE_WITH_KNOTS('',3,(#33291,#33292,#33293,#33294,#33295,
#33296,#33297,#33298,#33299,#33300,#33301,#33302,#33303,#33304,#33305,#33306,
#33307,#33308,#33309),.UNSPECIFIED.,.F.,.F.,(4,3,3,3,3,3,4),(-65.3636982725397,
-64.8849073156381,-63.8866779723206,-62.8884486290032,-61.8902192856856,
-60.8919899423681,-60.6406912850648),.UNSPECIFIED.);
#2361=B_SPLINE_CURVE_WITH_KNOTS('',3,(#33312,#33313,#33314,#33315,#33316,
#33317,#33318,#33319,#33320),.UNSPECIFIED.,.F.,.F.,(4,1,1,1,1,1,4),(10.375208827628,
11.3000595749863,12.2994007152123,13.2987418554383,14.2980829956642,15.2974241358902,
15.7079632679489),.UNSPECIFIED.);
#2362=B_SPLINE_CURVE_WITH_KNOTS('',3,(#33610,#33611,#33612,#33613,#33614,
#33615,#33616,#33617,#33618,#33619,#33620,#33621,#33622,#33623,#33624,#33625,
#33626,#33627,#33628,#33629,#33630,#33631),.UNSPECIFIED.,.F.,.F.,(4,3,3,
3,3,3,3,4),(57.6714095710772,57.9617861331071,58.961127273333,59.960468413559,
60.959809553785,61.959150694011,62.958491834237,63.29052559922),
 .UNSPECIFIED.);
#2363=B_SPLINE_CURVE_WITH_KNOTS('',3,(#33632,#33633,#33634,#33635,#33636,
#33637,#33638,#33639,#33640,#33641,#33642,#33643,#33644,#33645,#33646,#33647,
#33648,#33649,#33650,#33651,#33652,#33653,#33654,#33655,#33656,#33657,#33658,
#33659,#33660,#33661,#33662,#33663,#33664,#33665,#33666,#33667,#33668,#33669,
#33670,#33671,#33672,#33673,#33674,#33675,#33676,#33677,#33678,#33679,#33680,
#33681,#33682,#33683),.UNSPECIFIED.,.F.,.F.,(4,3,3,3,3,3,3,3,3,3,3,3,3,
3,3,3,3,4),(-0.276631791712725,-0.267716618892456,-0.246046101828633,-0.235289362386452,
-0.214941892616146,-0.204749662554743,-0.176256346031651,-0.161806307413905,
-0.15286753466007,-0.140652476775023,-0.120886137603943,-0.110226811379351,
-0.100669960776508,-0.0755024705823808,-0.058604244392821,-0.0491682800449266,
-0.0181536719473738,0.),.UNSPECIFIED.);
#2923=LINE('',#32057,#3497);
#2924=LINE('',#32081,#3498);
#2925=LINE('',#32129,#3499);
#2926=LINE('',#32177,#3500);
#2927=LINE('',#32225,#3501);
#2928=LINE('',#32279,#3502);
#2929=LINE('',#32327,#3503);
#2930=LINE('',#32375,#3504);
#2931=LINE('',#32429,#3505);
#2932=LINE('',#32477,#3506);
#2933=LINE('',#32525,#3507);
#2934=LINE('',#32551,#3508);
#2935=LINE('',#32575,#3509);
#2936=LINE('',#32599,#3510);
#2937=LINE('',#32624,#3511);
#2938=LINE('',#32649,#3512);
#2939=LINE('',#32673,#3513);
#2940=LINE('',#32698,#3514);
#2941=LINE('',#32723,#3515);
#2942=LINE('',#32747,#3516);
#2943=LINE('',#32951,#3517);
#2944=LINE('',#33688,#3518);
#2945=LINE('',#33690,#3519);
#2946=LINE('',#33692,#3520);
#2947=LINE('',#33693,#3521);
#2948=LINE('',#33696,#3522);
#2949=LINE('',#33698,#3523);
#2950=LINE('',#33699,#3524);
#2951=LINE('',#33702,#3525);
#2952=LINE('',#33704,#3526);
#2953=LINE('',#33705,#3527);
#2954=LINE('',#33708,#3528);
#2955=LINE('',#33710,#3529);
#2956=LINE('',#33711,#3530);
#2957=LINE('',#33714,#3531);
#2958=LINE('',#33716,#3532);
#2959=LINE('',#33717,#3533);
#2960=LINE('',#33719,#3534);
#2961=LINE('',#33720,#3535);
#2962=LINE('',#33727,#3536);
#3497=VECTOR('',#12346,0.15);
#3498=VECTOR('',#12351,0.15);
#3499=VECTOR('',#12354,0.15);
#3500=VECTOR('',#12357,0.15);
#3501=VECTOR('',#12360,0.15);
#3502=VECTOR('',#12363,0.15);
#3503=VECTOR('',#12366,0.15);
#3504=VECTOR('',#12369,0.15);
#3505=VECTOR('',#12372,0.15);
#3506=VECTOR('',#12375,0.15);
#3507=VECTOR('',#12378,0.117775);
#3508=VECTOR('',#12383,0.117775);
#3509=VECTOR('',#12386,0.117775);
#3510=VECTOR('',#12389,0.117775);
#3511=VECTOR('',#12392,0.117775);
#3512=VECTOR('',#12395,0.117775);
#3513=VECTOR('',#12398,0.117775);
#3514=VECTOR('',#12401,0.117775);
#3515=VECTOR('',#12404,0.117775);
#3516=VECTOR('',#12407,0.117775);
#3517=VECTOR('',#12412,0.1);
#3518=VECTOR('',#12423,1.);
#3519=VECTOR('',#12424,1.);
#3520=VECTOR('',#12425,1.);
#3521=VECTOR('',#12426,1.);
#3522=VECTOR('',#12429,1.);
#3523=VECTOR('',#12430,1.);
#3524=VECTOR('',#12431,1.);
#3525=VECTOR('',#12434,1.);
#3526=VECTOR('',#12435,1.);
#3527=VECTOR('',#12436,1.);
#3528=VECTOR('',#12439,1.);
#3529=VECTOR('',#12440,1.);
#3530=VECTOR('',#12441,1.);
#3531=VECTOR('',#12444,1.);
#3532=VECTOR('',#12445,1.);
#3533=VECTOR('',#12446,1.);
#3534=VECTOR('',#12449,1.);
#3535=VECTOR('',#12450,1.);
#3536=VECTOR('',#12459,0.3);
#4389=VERTEX_POINT('',#32055);
#4390=VERTEX_POINT('',#32056);
#4391=VERTEX_POINT('',#32058);
#4392=VERTEX_POINT('',#32069);
#4393=VERTEX_POINT('',#32079);
#4394=VERTEX_POINT('',#32080);
#4395=VERTEX_POINT('',#32127);
#4396=VERTEX_POINT('',#32128);
#4397=VERTEX_POINT('',#32175);
#4398=VERTEX_POINT('',#32176);
#4399=VERTEX_POINT('',#32223);
#4400=VERTEX_POINT('',#32224);
#4401=VERTEX_POINT('',#32277);
#4402=VERTEX_POINT('',#32278);
#4403=VERTEX_POINT('',#32325);
#4404=VERTEX_POINT('',#32326);
#4405=VERTEX_POINT('',#32373);
#4406=VERTEX_POINT('',#32374);
#4407=VERTEX_POINT('',#32427);
#4408=VERTEX_POINT('',#32428);
#4409=VERTEX_POINT('',#32475);
#4410=VERTEX_POINT('',#32476);
#4411=VERTEX_POINT('',#32523);
#4412=VERTEX_POINT('',#32524);
#4413=VERTEX_POINT('',#32526);
#4414=VERTEX_POINT('',#32537);
#4415=VERTEX_POINT('',#32549);
#4416=VERTEX_POINT('',#32550);
#4417=VERTEX_POINT('',#32573);
#4418=VERTEX_POINT('',#32574);
#4419=VERTEX_POINT('',#32597);
#4420=VERTEX_POINT('',#32598);
#4421=VERTEX_POINT('',#32622);
#4422=VERTEX_POINT('',#32623);
#4423=VERTEX_POINT('',#32647);
#4424=VERTEX_POINT('',#32648);
#4425=VERTEX_POINT('',#32671);
#4426=VERTEX_POINT('',#32672);
#4427=VERTEX_POINT('',#32696);
#4428=VERTEX_POINT('',#32697);
#4429=VERTEX_POINT('',#32721);
#4430=VERTEX_POINT('',#32722);
#4431=VERTEX_POINT('',#32745);
#4432=VERTEX_POINT('',#32746);
#4433=VERTEX_POINT('',#32769);
#4434=VERTEX_POINT('',#32894);
#4435=VERTEX_POINT('',#32932);
#4436=VERTEX_POINT('',#32950);
#4437=VERTEX_POINT('',#33233);
#4438=VERTEX_POINT('',#33311);
#4439=VERTEX_POINT('',#33686);
#4440=VERTEX_POINT('',#33687);
#4441=VERTEX_POINT('',#33689);
#4442=VERTEX_POINT('',#33691);
#4443=VERTEX_POINT('',#33695);
#4444=VERTEX_POINT('',#33697);
#4445=VERTEX_POINT('',#33701);
#4446=VERTEX_POINT('',#33703);
#4447=VERTEX_POINT('',#33707);
#4448=VERTEX_POINT('',#33709);
#4449=VERTEX_POINT('',#33713);
#4450=VERTEX_POINT('',#33715);
#4451=VERTEX_POINT('',#33723);
#4452=VERTEX_POINT('',#33726);
#5746=EDGE_CURVE('',#4389,#4390,#2923,.T.);
#5747=EDGE_CURVE('',#4389,#4391,#2315,.T.);
#5748=EDGE_CURVE('',#4391,#4392,#1724,.F.);
#5749=EDGE_CURVE('',#4392,#4390,#2316,.T.);
#5750=EDGE_CURVE('',#4393,#4394,#2924,.T.);
#5751=EDGE_CURVE('',#4393,#4389,#2317,.T.);
#5752=EDGE_CURVE('',#4390,#4394,#2318,.T.);
#5753=EDGE_CURVE('',#4395,#4396,#2925,.T.);
#5754=EDGE_CURVE('',#4395,#4393,#2319,.T.);
#5755=EDGE_CURVE('',#4394,#4396,#2320,.T.);
#5756=EDGE_CURVE('',#4397,#4398,#2926,.T.);
#5757=EDGE_CURVE('',#4397,#4395,#2321,.T.);
#5758=EDGE_CURVE('',#4396,#4398,#2322,.T.);
#5759=EDGE_CURVE('',#4399,#4400,#2927,.T.);
#5760=EDGE_CURVE('',#4399,#4397,#2323,.T.);
#5761=EDGE_CURVE('',#4398,#4400,#2324,.T.);
#5762=EDGE_CURVE('',#4401,#4402,#2928,.T.);
#5763=EDGE_CURVE('',#4401,#4399,#2325,.T.);
#5764=EDGE_CURVE('',#4400,#4402,#2326,.T.);
#5765=EDGE_CURVE('',#4403,#4404,#2929,.T.);
#5766=EDGE_CURVE('',#4403,#4401,#2327,.T.);
#5767=EDGE_CURVE('',#4402,#4404,#2328,.T.);
#5768=EDGE_CURVE('',#4405,#4406,#2930,.T.);
#5769=EDGE_CURVE('',#4405,#4403,#2329,.T.);
#5770=EDGE_CURVE('',#4404,#4406,#2330,.T.);
#5771=EDGE_CURVE('',#4407,#4408,#2931,.T.);
#5772=EDGE_CURVE('',#4407,#4405,#2331,.T.);
#5773=EDGE_CURVE('',#4406,#4408,#2332,.T.);
#5774=EDGE_CURVE('',#4409,#4410,#2932,.T.);
#5775=EDGE_CURVE('',#4409,#4407,#2333,.T.);
#5776=EDGE_CURVE('',#4408,#4410,#2334,.T.);
#5777=EDGE_CURVE('',#4411,#4412,#2933,.T.);
#5778=EDGE_CURVE('',#4411,#4413,#2335,.T.);
#5779=EDGE_CURVE('',#4413,#4414,#1725,.T.);
#5780=EDGE_CURVE('',#4412,#4414,#2336,.T.);
#5781=EDGE_CURVE('',#4415,#4416,#2934,.T.);
#5782=EDGE_CURVE('',#4415,#4411,#2337,.T.);
#5783=EDGE_CURVE('',#4416,#4412,#2338,.T.);
#5784=EDGE_CURVE('',#4417,#4418,#2935,.T.);
#5785=EDGE_CURVE('',#4417,#4415,#2339,.T.);
#5786=EDGE_CURVE('',#4418,#4416,#2340,.T.);
#5787=EDGE_CURVE('',#4419,#4420,#2936,.T.);
#5788=EDGE_CURVE('',#4419,#4417,#2341,.T.);
#5789=EDGE_CURVE('',#4420,#4418,#2342,.T.);
#5790=EDGE_CURVE('',#4421,#4422,#2937,.T.);
#5791=EDGE_CURVE('',#4421,#4419,#2343,.T.);
#5792=EDGE_CURVE('',#4422,#4420,#2344,.T.);
#5793=EDGE_CURVE('',#4423,#4424,#2938,.T.);
#5794=EDGE_CURVE('',#4423,#4421,#2345,.T.);
#5795=EDGE_CURVE('',#4424,#4422,#2346,.T.);
#5796=EDGE_CURVE('',#4425,#4426,#2939,.T.);
#5797=EDGE_CURVE('',#4425,#4423,#2347,.T.);
#5798=EDGE_CURVE('',#4426,#4424,#2348,.T.);
#5799=EDGE_CURVE('',#4427,#4428,#2940,.T.);
#5800=EDGE_CURVE('',#4427,#4425,#2349,.T.);
#5801=EDGE_CURVE('',#4428,#4426,#2350,.T.);
#5802=EDGE_CURVE('',#4429,#4430,#2941,.T.);
#5803=EDGE_CURVE('',#4429,#4427,#2351,.T.);
#5804=EDGE_CURVE('',#4430,#4428,#2352,.T.);
#5805=EDGE_CURVE('',#4431,#4432,#2942,.T.);
#5806=EDGE_CURVE('',#4431,#4429,#2353,.T.);
#5807=EDGE_CURVE('',#4432,#4430,#2354,.T.);
#5808=EDGE_CURVE('',#4414,#4433,#2355,.T.);
#5809=EDGE_CURVE('',#4434,#4413,#2356,.T.);
#5810=EDGE_CURVE('',#4435,#4434,#1726,.T.);
#5811=EDGE_CURVE('',#4433,#4435,#2357,.T.);
#5812=EDGE_CURVE('',#4433,#4436,#2943,.T.);
#5813=EDGE_CURVE('',#4436,#4436,#1727,.T.);
#5814=EDGE_CURVE('',#4437,#4431,#2358,.T.);
#5815=EDGE_CURVE('',#4391,#4437,#2359,.T.);
#5816=EDGE_CURVE('',#4434,#4409,#2360,.T.);
#5817=EDGE_CURVE('',#4438,#4432,#2361,.T.);
#5818=EDGE_CURVE('',#4437,#4438,#1728,.T.);
#5819=EDGE_CURVE('',#4410,#4435,#2362,.T.);
#5820=EDGE_CURVE('',#4438,#4392,#2363,.T.);
#5821=EDGE_CURVE('',#4439,#4440,#2944,.T.);
#5822=EDGE_CURVE('',#4439,#4441,#2945,.T.);
#5823=EDGE_CURVE('',#4441,#4442,#2946,.T.);
#5824=EDGE_CURVE('',#4440,#4442,#2947,.T.);
#5825=EDGE_CURVE('',#4443,#4439,#2948,.T.);
#5826=EDGE_CURVE('',#4443,#4444,#2949,.T.);
#5827=EDGE_CURVE('',#4444,#4441,#2950,.T.);
#5828=EDGE_CURVE('',#4445,#4443,#2951,.T.);
#5829=EDGE_CURVE('',#4445,#4446,#2952,.T.);
#5830=EDGE_CURVE('',#4446,#4444,#2953,.T.);
#5831=EDGE_CURVE('',#4447,#4445,#2954,.T.);
#5832=EDGE_CURVE('',#4447,#4448,#2955,.T.);
#5833=EDGE_CURVE('',#4448,#4446,#2956,.T.);
#5834=EDGE_CURVE('',#4449,#4447,#2957,.T.);
#5835=EDGE_CURVE('',#4449,#4450,#2958,.T.);
#5836=EDGE_CURVE('',#4450,#4448,#2959,.T.);
#5837=EDGE_CURVE('',#4440,#4449,#2960,.T.);
#5838=EDGE_CURVE('',#4442,#4450,#2961,.T.);
#5839=EDGE_CURVE('',#4451,#4451,#1729,.T.);
#5840=EDGE_CURVE('',#4451,#4452,#2962,.T.);
#5841=EDGE_CURVE('',#4452,#4452,#1730,.T.);
#8380=ORIENTED_EDGE('',*,*,#5746,.F.);
#8381=ORIENTED_EDGE('',*,*,#5747,.T.);
#8382=ORIENTED_EDGE('',*,*,#5748,.T.);
#8383=ORIENTED_EDGE('',*,*,#5749,.T.);
#8384=ORIENTED_EDGE('',*,*,#5750,.F.);
#8385=ORIENTED_EDGE('',*,*,#5751,.T.);
#8386=ORIENTED_EDGE('',*,*,#5746,.T.);
#8387=ORIENTED_EDGE('',*,*,#5752,.T.);
#8388=ORIENTED_EDGE('',*,*,#5753,.F.);
#8389=ORIENTED_EDGE('',*,*,#5754,.T.);
#8390=ORIENTED_EDGE('',*,*,#5750,.T.);
#8391=ORIENTED_EDGE('',*,*,#5755,.T.);
#8392=ORIENTED_EDGE('',*,*,#5756,.F.);
#8393=ORIENTED_EDGE('',*,*,#5757,.T.);
#8394=ORIENTED_EDGE('',*,*,#5753,.T.);
#8395=ORIENTED_EDGE('',*,*,#5758,.T.);
#8396=ORIENTED_EDGE('',*,*,#5759,.F.);
#8397=ORIENTED_EDGE('',*,*,#5760,.T.);
#8398=ORIENTED_EDGE('',*,*,#5756,.T.);
#8399=ORIENTED_EDGE('',*,*,#5761,.T.);
#8400=ORIENTED_EDGE('',*,*,#5762,.F.);
#8401=ORIENTED_EDGE('',*,*,#5763,.T.);
#8402=ORIENTED_EDGE('',*,*,#5759,.T.);
#8403=ORIENTED_EDGE('',*,*,#5764,.T.);
#8404=ORIENTED_EDGE('',*,*,#5765,.F.);
#8405=ORIENTED_EDGE('',*,*,#5766,.T.);
#8406=ORIENTED_EDGE('',*,*,#5762,.T.);
#8407=ORIENTED_EDGE('',*,*,#5767,.T.);
#8408=ORIENTED_EDGE('',*,*,#5768,.F.);
#8409=ORIENTED_EDGE('',*,*,#5769,.T.);
#8410=ORIENTED_EDGE('',*,*,#5765,.T.);
#8411=ORIENTED_EDGE('',*,*,#5770,.T.);
#8412=ORIENTED_EDGE('',*,*,#5771,.F.);
#8413=ORIENTED_EDGE('',*,*,#5772,.T.);
#8414=ORIENTED_EDGE('',*,*,#5768,.T.);
#8415=ORIENTED_EDGE('',*,*,#5773,.T.);
#8416=ORIENTED_EDGE('',*,*,#5774,.F.);
#8417=ORIENTED_EDGE('',*,*,#5775,.T.);
#8418=ORIENTED_EDGE('',*,*,#5771,.T.);
#8419=ORIENTED_EDGE('',*,*,#5776,.T.);
#8420=ORIENTED_EDGE('',*,*,#5777,.F.);
#8421=ORIENTED_EDGE('',*,*,#5778,.T.);
#8422=ORIENTED_EDGE('',*,*,#5779,.T.);
#8423=ORIENTED_EDGE('',*,*,#5780,.F.);
#8424=ORIENTED_EDGE('',*,*,#5781,.F.);
#8425=ORIENTED_EDGE('',*,*,#5782,.T.);
#8426=ORIENTED_EDGE('',*,*,#5777,.T.);
#8427=ORIENTED_EDGE('',*,*,#5783,.F.);
#8428=ORIENTED_EDGE('',*,*,#5784,.F.);
#8429=ORIENTED_EDGE('',*,*,#5785,.T.);
#8430=ORIENTED_EDGE('',*,*,#5781,.T.);
#8431=ORIENTED_EDGE('',*,*,#5786,.F.);
#8432=ORIENTED_EDGE('',*,*,#5787,.F.);
#8433=ORIENTED_EDGE('',*,*,#5788,.T.);
#8434=ORIENTED_EDGE('',*,*,#5784,.T.);
#8435=ORIENTED_EDGE('',*,*,#5789,.F.);
#8436=ORIENTED_EDGE('',*,*,#5790,.F.);
#8437=ORIENTED_EDGE('',*,*,#5791,.T.);
#8438=ORIENTED_EDGE('',*,*,#5787,.T.);
#8439=ORIENTED_EDGE('',*,*,#5792,.F.);
#8440=ORIENTED_EDGE('',*,*,#5793,.F.);
#8441=ORIENTED_EDGE('',*,*,#5794,.T.);
#8442=ORIENTED_EDGE('',*,*,#5790,.T.);
#8443=ORIENTED_EDGE('',*,*,#5795,.F.);
#8444=ORIENTED_EDGE('',*,*,#5796,.F.);
#8445=ORIENTED_EDGE('',*,*,#5797,.T.);
#8446=ORIENTED_EDGE('',*,*,#5793,.T.);
#8447=ORIENTED_EDGE('',*,*,#5798,.F.);
#8448=ORIENTED_EDGE('',*,*,#5799,.F.);
#8449=ORIENTED_EDGE('',*,*,#5800,.T.);
#8450=ORIENTED_EDGE('',*,*,#5796,.T.);
#8451=ORIENTED_EDGE('',*,*,#5801,.F.);
#8452=ORIENTED_EDGE('',*,*,#5802,.F.);
#8453=ORIENTED_EDGE('',*,*,#5803,.T.);
#8454=ORIENTED_EDGE('',*,*,#5799,.T.);
#8455=ORIENTED_EDGE('',*,*,#5804,.F.);
#8456=ORIENTED_EDGE('',*,*,#5805,.F.);
#8457=ORIENTED_EDGE('',*,*,#5806,.T.);
#8458=ORIENTED_EDGE('',*,*,#5802,.T.);
#8459=ORIENTED_EDGE('',*,*,#5807,.F.);
#8460=ORIENTED_EDGE('',*,*,#5808,.F.);
#8461=ORIENTED_EDGE('',*,*,#5779,.F.);
#8462=ORIENTED_EDGE('',*,*,#5809,.F.);
#8463=ORIENTED_EDGE('',*,*,#5810,.F.);
#8464=ORIENTED_EDGE('',*,*,#5811,.F.);
#8465=ORIENTED_EDGE('',*,*,#5812,.T.);
#8466=ORIENTED_EDGE('',*,*,#5813,.F.);
#8467=ORIENTED_EDGE('',*,*,#5812,.F.);
#8468=ORIENTED_EDGE('',*,*,#5809,.T.);
#8469=ORIENTED_EDGE('',*,*,#5778,.F.);
#8470=ORIENTED_EDGE('',*,*,#5782,.F.);
#8471=ORIENTED_EDGE('',*,*,#5785,.F.);
#8472=ORIENTED_EDGE('',*,*,#5788,.F.);
#8473=ORIENTED_EDGE('',*,*,#5791,.F.);
#8474=ORIENTED_EDGE('',*,*,#5794,.F.);
#8475=ORIENTED_EDGE('',*,*,#5797,.F.);
#8476=ORIENTED_EDGE('',*,*,#5800,.F.);
#8477=ORIENTED_EDGE('',*,*,#5803,.F.);
#8478=ORIENTED_EDGE('',*,*,#5806,.F.);
#8479=ORIENTED_EDGE('',*,*,#5814,.F.);
#8480=ORIENTED_EDGE('',*,*,#5815,.F.);
#8481=ORIENTED_EDGE('',*,*,#5747,.F.);
#8482=ORIENTED_EDGE('',*,*,#5751,.F.);
#8483=ORIENTED_EDGE('',*,*,#5754,.F.);
#8484=ORIENTED_EDGE('',*,*,#5757,.F.);
#8485=ORIENTED_EDGE('',*,*,#5760,.F.);
#8486=ORIENTED_EDGE('',*,*,#5763,.F.);
#8487=ORIENTED_EDGE('',*,*,#5766,.F.);
#8488=ORIENTED_EDGE('',*,*,#5769,.F.);
#8489=ORIENTED_EDGE('',*,*,#5772,.F.);
#8490=ORIENTED_EDGE('',*,*,#5775,.F.);
#8491=ORIENTED_EDGE('',*,*,#5816,.F.);
#8492=ORIENTED_EDGE('',*,*,#5805,.T.);
#8493=ORIENTED_EDGE('',*,*,#5817,.F.);
#8494=ORIENTED_EDGE('',*,*,#5818,.F.);
#8495=ORIENTED_EDGE('',*,*,#5814,.T.);
#8496=ORIENTED_EDGE('',*,*,#5808,.T.);
#8497=ORIENTED_EDGE('',*,*,#5811,.T.);
#8498=ORIENTED_EDGE('',*,*,#5819,.F.);
#8499=ORIENTED_EDGE('',*,*,#5776,.F.);
#8500=ORIENTED_EDGE('',*,*,#5773,.F.);
#8501=ORIENTED_EDGE('',*,*,#5770,.F.);
#8502=ORIENTED_EDGE('',*,*,#5767,.F.);
#8503=ORIENTED_EDGE('',*,*,#5764,.F.);
#8504=ORIENTED_EDGE('',*,*,#5761,.F.);
#8505=ORIENTED_EDGE('',*,*,#5758,.F.);
#8506=ORIENTED_EDGE('',*,*,#5755,.F.);
#8507=ORIENTED_EDGE('',*,*,#5752,.F.);
#8508=ORIENTED_EDGE('',*,*,#5749,.F.);
#8509=ORIENTED_EDGE('',*,*,#5820,.F.);
#8510=ORIENTED_EDGE('',*,*,#5817,.T.);
#8511=ORIENTED_EDGE('',*,*,#5807,.T.);
#8512=ORIENTED_EDGE('',*,*,#5804,.T.);
#8513=ORIENTED_EDGE('',*,*,#5801,.T.);
#8514=ORIENTED_EDGE('',*,*,#5798,.T.);
#8515=ORIENTED_EDGE('',*,*,#5795,.T.);
#8516=ORIENTED_EDGE('',*,*,#5792,.T.);
#8517=ORIENTED_EDGE('',*,*,#5789,.T.);
#8518=ORIENTED_EDGE('',*,*,#5786,.T.);
#8519=ORIENTED_EDGE('',*,*,#5783,.T.);
#8520=ORIENTED_EDGE('',*,*,#5780,.T.);
#8521=ORIENTED_EDGE('',*,*,#5774,.T.);
#8522=ORIENTED_EDGE('',*,*,#5819,.T.);
#8523=ORIENTED_EDGE('',*,*,#5810,.T.);
#8524=ORIENTED_EDGE('',*,*,#5816,.T.);
#8525=ORIENTED_EDGE('',*,*,#5821,.F.);
#8526=ORIENTED_EDGE('',*,*,#5822,.T.);
#8527=ORIENTED_EDGE('',*,*,#5823,.T.);
#8528=ORIENTED_EDGE('',*,*,#5824,.F.);
#8529=ORIENTED_EDGE('',*,*,#5825,.F.);
#8530=ORIENTED_EDGE('',*,*,#5826,.T.);
#8531=ORIENTED_EDGE('',*,*,#5827,.T.);
#8532=ORIENTED_EDGE('',*,*,#5822,.F.);
#8533=ORIENTED_EDGE('',*,*,#5828,.F.);
#8534=ORIENTED_EDGE('',*,*,#5829,.T.);
#8535=ORIENTED_EDGE('',*,*,#5830,.T.);
#8536=ORIENTED_EDGE('',*,*,#5826,.F.);
#8537=ORIENTED_EDGE('',*,*,#5831,.F.);
#8538=ORIENTED_EDGE('',*,*,#5832,.T.);
#8539=ORIENTED_EDGE('',*,*,#5833,.T.);
#8540=ORIENTED_EDGE('',*,*,#5829,.F.);
#8541=ORIENTED_EDGE('',*,*,#5834,.F.);
#8542=ORIENTED_EDGE('',*,*,#5835,.T.);
#8543=ORIENTED_EDGE('',*,*,#5836,.T.);
#8544=ORIENTED_EDGE('',*,*,#5832,.F.);
#8545=ORIENTED_EDGE('',*,*,#5837,.F.);
#8546=ORIENTED_EDGE('',*,*,#5824,.T.);
#8547=ORIENTED_EDGE('',*,*,#5838,.T.);
#8548=ORIENTED_EDGE('',*,*,#5835,.F.);
#8549=ORIENTED_EDGE('',*,*,#5838,.F.);
#8550=ORIENTED_EDGE('',*,*,#5823,.F.);
#8551=ORIENTED_EDGE('',*,*,#5827,.F.);
#8552=ORIENTED_EDGE('',*,*,#5830,.F.);
#8553=ORIENTED_EDGE('',*,*,#5833,.F.);
#8554=ORIENTED_EDGE('',*,*,#5836,.F.);
#8555=ORIENTED_EDGE('',*,*,#5839,.T.);
#8556=ORIENTED_EDGE('',*,*,#5815,.T.);
#8557=ORIENTED_EDGE('',*,*,#5818,.T.);
#8558=ORIENTED_EDGE('',*,*,#5820,.T.);
#8559=ORIENTED_EDGE('',*,*,#5748,.F.);
#8560=ORIENTED_EDGE('',*,*,#5839,.F.);
#8561=ORIENTED_EDGE('',*,*,#5840,.T.);
#8562=ORIENTED_EDGE('',*,*,#5841,.T.);
#8563=ORIENTED_EDGE('',*,*,#5840,.F.);
#8564=ORIENTED_EDGE('',*,*,#5841,.F.);
#8565=ORIENTED_EDGE('',*,*,#5821,.T.);
#8566=ORIENTED_EDGE('',*,*,#5837,.T.);
#8567=ORIENTED_EDGE('',*,*,#5834,.T.);
#8568=ORIENTED_EDGE('',*,*,#5831,.T.);
#8569=ORIENTED_EDGE('',*,*,#5828,.T.);
#8570=ORIENTED_EDGE('',*,*,#5825,.T.);
#8571=ORIENTED_EDGE('',*,*,#5813,.T.);
#9167=CYLINDRICAL_SURFACE('',#10560,0.14635);
#9168=CYLINDRICAL_SURFACE('',#10562,0.14635);
#9169=CYLINDRICAL_SURFACE('',#10563,0.14635);
#9170=CYLINDRICAL_SURFACE('',#10564,0.14635);
#9171=CYLINDRICAL_SURFACE('',#10565,0.14635);
#9172=CYLINDRICAL_SURFACE('',#10566,0.14635);
#9173=CYLINDRICAL_SURFACE('',#10567,0.14635);
#9174=CYLINDRICAL_SURFACE('',#10568,0.14635);
#9175=CYLINDRICAL_SURFACE('',#10569,0.14635);
#9176=CYLINDRICAL_SURFACE('',#10570,0.14635);
#9177=CYLINDRICAL_SURFACE('',#10571,0.117775);
#9178=CYLINDRICAL_SURFACE('',#10573,0.117775);
#9179=CYLINDRICAL_SURFACE('',#10574,0.117775);
#9180=CYLINDRICAL_SURFACE('',#10575,0.117775);
#9181=CYLINDRICAL_SURFACE('',#10576,0.117775);
#9182=CYLINDRICAL_SURFACE('',#10577,0.117775);
#9183=CYLINDRICAL_SURFACE('',#10578,0.117775);
#9184=CYLINDRICAL_SURFACE('',#10579,0.117775);
#9185=CYLINDRICAL_SURFACE('',#10580,0.117775);
#9186=CYLINDRICAL_SURFACE('',#10581,0.117775);
#9187=CYLINDRICAL_SURFACE('',#10585,0.117775);
#9188=CYLINDRICAL_SURFACE('',#10587,0.14635);
#9189=CYLINDRICAL_SURFACE('',#10597,0.3);
#9679=ADVANCED_FACE('',(#889),#9167,.T.);
#9680=ADVANCED_FACE('',(#890),#9168,.T.);
#9681=ADVANCED_FACE('',(#891),#9169,.T.);
#9682=ADVANCED_FACE('',(#892),#9170,.T.);
#9683=ADVANCED_FACE('',(#893),#9171,.T.);
#9684=ADVANCED_FACE('',(#894),#9172,.T.);
#9685=ADVANCED_FACE('',(#895),#9173,.T.);
#9686=ADVANCED_FACE('',(#896),#9174,.T.);
#9687=ADVANCED_FACE('',(#897),#9175,.T.);
#9688=ADVANCED_FACE('',(#898),#9176,.T.);
#9689=ADVANCED_FACE('',(#899),#9177,.T.);
#9690=ADVANCED_FACE('',(#900),#9178,.T.);
#9691=ADVANCED_FACE('',(#901),#9179,.T.);
#9692=ADVANCED_FACE('',(#902),#9180,.T.);
#9693=ADVANCED_FACE('',(#903),#9181,.T.);
#9694=ADVANCED_FACE('',(#904),#9182,.T.);
#9695=ADVANCED_FACE('',(#905),#9183,.T.);
#9696=ADVANCED_FACE('',(#906),#9184,.T.);
#9697=ADVANCED_FACE('',(#907),#9185,.T.);
#9698=ADVANCED_FACE('',(#908),#9186,.T.);
#9699=ADVANCED_FACE('',(#909),#140,.T.);
#9700=ADVANCED_FACE('',(#910),#231,.F.);
#9701=ADVANCED_FACE('',(#911),#9187,.T.);
#9702=ADVANCED_FACE('',(#912),#232,.F.);
#9703=ADVANCED_FACE('',(#913),#9188,.T.);
#9704=ADVANCED_FACE('',(#914),#419,.F.);
#9705=ADVANCED_FACE('',(#915),#420,.F.);
#9706=ADVANCED_FACE('',(#916),#421,.F.);
#9707=ADVANCED_FACE('',(#917),#422,.F.);
#9708=ADVANCED_FACE('',(#918),#423,.F.);
#9709=ADVANCED_FACE('',(#919),#424,.F.);
#9710=ADVANCED_FACE('',(#920),#425,.F.);
#9711=ADVANCED_FACE('',(#921,#298),#426,.T.);
#9712=ADVANCED_FACE('',(#922),#9189,.T.);
#9713=ADVANCED_FACE('',(#923,#299),#427,.F.);
#9714=ADVANCED_FACE('',(#924),#428,.T.);
#9782=CLOSED_SHELL('',(#9679,#9680,#9681,#9682,#9683,#9684,#9685,#9686,
#9687,#9688,#9689,#9690,#9691,#9692,#9693,#9694,#9695,#9696,#9697,#9698,
#9699,#9700,#9701,#9702,#9703,#9704,#9705,#9706,#9707,#9708,#9709,#9710,
#9711,#9712,#9713,#9714));
#10559=AXIS2_PLACEMENT_3D('',#32053,#12342,#12343);
#10560=AXIS2_PLACEMENT_3D('',#32054,#12344,#12345);
#10561=AXIS2_PLACEMENT_3D('',#32070,#12347,#12348);
#10562=AXIS2_PLACEMENT_3D('',#32078,#12349,#12350);
#10563=AXIS2_PLACEMENT_3D('',#32126,#12352,#12353);
#10564=AXIS2_PLACEMENT_3D('',#32174,#12355,#12356);
#10565=AXIS2_PLACEMENT_3D('',#32222,#12358,#12359);
#10566=AXIS2_PLACEMENT_3D('',#32276,#12361,#12362);
#10567=AXIS2_PLACEMENT_3D('',#32324,#12364,#12365);
#10568=AXIS2_PLACEMENT_3D('',#32372,#12367,#12368);
#10569=AXIS2_PLACEMENT_3D('',#32426,#12370,#12371);
#10570=AXIS2_PLACEMENT_3D('',#32474,#12373,#12374);
#10571=AXIS2_PLACEMENT_3D('',#32522,#12376,#12377);
#10572=AXIS2_PLACEMENT_3D('',#32538,#12379,#12380);
#10573=AXIS2_PLACEMENT_3D('',#32548,#12381,#12382);
#10574=AXIS2_PLACEMENT_3D('',#32572,#12384,#12385);
#10575=AXIS2_PLACEMENT_3D('',#32596,#12387,#12388);
#10576=AXIS2_PLACEMENT_3D('',#32621,#12390,#12391);
#10577=AXIS2_PLACEMENT_3D('',#32646,#12393,#12394);
#10578=AXIS2_PLACEMENT_3D('',#32670,#12396,#12397);
#10579=AXIS2_PLACEMENT_3D('',#32695,#12399,#12400);
#10580=AXIS2_PLACEMENT_3D('',#32720,#12402,#12403);
#10581=AXIS2_PLACEMENT_3D('',#32744,#12405,#12406);
#10582=AXIS2_PLACEMENT_3D('',#32768,#12408,#12409);
#10583=AXIS2_PLACEMENT_3D('',#32933,#12410,#12411);
#10584=AXIS2_PLACEMENT_3D('',#32952,#12413,#12414);
#10585=AXIS2_PLACEMENT_3D('',#33310,#12415,#12416);
#10586=AXIS2_PLACEMENT_3D('',#33321,#12417,#12418);
#10587=AXIS2_PLACEMENT_3D('',#33684,#12419,#12420);
#10588=AXIS2_PLACEMENT_3D('',#33685,#12421,#12422);
#10589=AXIS2_PLACEMENT_3D('',#33694,#12427,#12428);
#10590=AXIS2_PLACEMENT_3D('',#33700,#12432,#12433);
#10591=AXIS2_PLACEMENT_3D('',#33706,#12437,#12438);
#10592=AXIS2_PLACEMENT_3D('',#33712,#12442,#12443);
#10593=AXIS2_PLACEMENT_3D('',#33718,#12447,#12448);
#10594=AXIS2_PLACEMENT_3D('',#33721,#12451,#12452);
#10595=AXIS2_PLACEMENT_3D('',#33722,#12453,#12454);
#10596=AXIS2_PLACEMENT_3D('',#33724,#12455,#12456);
#10597=AXIS2_PLACEMENT_3D('',#33725,#12457,#12458);
#10598=AXIS2_PLACEMENT_3D('',#33728,#12460,#12461);
#10599=AXIS2_PLACEMENT_3D('',#33729,#12462,#12463);
#10600=AXIS2_PLACEMENT_3D('',#33730,#12464,#12465);
#12342=DIRECTION('axis',(0.,0.,1.));
#12343=DIRECTION('refdir',(1.,0.,0.));
#12344=DIRECTION('center_axis',(0.,0.,1.));
#12345=DIRECTION('ref_axis',(1.,0.,0.));
#12346=DIRECTION('',(0.,0.,-1.));
#12347=DIRECTION('center_axis',(0.,0.,-1.));
#12348=DIRECTION('ref_axis',(1.,0.,0.));
#12349=DIRECTION('center_axis',(0.,0.,1.));
#12350=DIRECTION('ref_axis',(1.,0.,0.));
#12351=DIRECTION('',(0.,0.,-1.));
#12352=DIRECTION('center_axis',(0.,0.,1.));
#12353=DIRECTION('ref_axis',(1.,0.,0.));
#12354=DIRECTION('',(0.,0.,-1.));
#12355=DIRECTION('center_axis',(0.,0.,1.));
#12356=DIRECTION('ref_axis',(1.,0.,0.));
#12357=DIRECTION('',(0.,0.,-1.));
#12358=DIRECTION('center_axis',(0.,0.,1.));
#12359=DIRECTION('ref_axis',(1.,0.,0.));
#12360=DIRECTION('',(0.,0.,-1.));
#12361=DIRECTION('center_axis',(0.,0.,1.));
#12362=DIRECTION('ref_axis',(1.,0.,0.));
#12363=DIRECTION('',(0.,0.,-1.));
#12364=DIRECTION('center_axis',(0.,0.,1.));
#12365=DIRECTION('ref_axis',(1.,0.,0.));
#12366=DIRECTION('',(0.,0.,-1.));
#12367=DIRECTION('center_axis',(0.,0.,1.));
#12368=DIRECTION('ref_axis',(1.,0.,0.));
#12369=DIRECTION('',(0.,0.,-1.));
#12370=DIRECTION('center_axis',(0.,0.,1.));
#12371=DIRECTION('ref_axis',(1.,0.,0.));
#12372=DIRECTION('',(0.,0.,-1.));
#12373=DIRECTION('center_axis',(0.,0.,1.));
#12374=DIRECTION('ref_axis',(1.,0.,0.));
#12375=DIRECTION('',(0.,0.,-1.));
#12376=DIRECTION('center_axis',(0.,0.,1.));
#12377=DIRECTION('ref_axis',(1.,7.53540174823413E-14,0.));
#12378=DIRECTION('',(0.,0.,1.));
#12379=DIRECTION('center_axis',(0.,0.,-1.));
#12380=DIRECTION('ref_axis',(1.,7.53540174823413E-14,0.));
#12381=DIRECTION('center_axis',(0.,0.,1.));
#12382=DIRECTION('ref_axis',(1.,7.53540174823413E-14,0.));
#12383=DIRECTION('',(0.,0.,1.));
#12384=DIRECTION('center_axis',(0.,0.,1.));
#12385=DIRECTION('ref_axis',(1.,7.53540174823413E-14,0.));
#12386=DIRECTION('',(0.,0.,1.));
#12387=DIRECTION('center_axis',(0.,0.,1.));
#12388=DIRECTION('ref_axis',(1.,7.53540174823413E-14,0.));
#12389=DIRECTION('',(0.,0.,1.));
#12390=DIRECTION('center_axis',(0.,0.,1.));
#12391=DIRECTION('ref_axis',(1.,7.53540174823413E-14,0.));
#12392=DIRECTION('',(0.,0.,1.));
#12393=DIRECTION('center_axis',(0.,0.,1.));
#12394=DIRECTION('ref_axis',(1.,7.53540174823413E-14,0.));
#12395=DIRECTION('',(0.,0.,1.));
#12396=DIRECTION('center_axis',(0.,0.,1.));
#12397=DIRECTION('ref_axis',(1.,7.53540174823413E-14,0.));
#12398=DIRECTION('',(0.,0.,1.));
#12399=DIRECTION('center_axis',(0.,0.,1.));
#12400=DIRECTION('ref_axis',(1.,7.53540174823413E-14,0.));
#12401=DIRECTION('',(0.,0.,1.));
#12402=DIRECTION('center_axis',(0.,0.,1.));
#12403=DIRECTION('ref_axis',(1.,7.53540174823413E-14,0.));
#12404=DIRECTION('',(0.,0.,1.));
#12405=DIRECTION('center_axis',(0.,0.,1.));
#12406=DIRECTION('ref_axis',(1.,7.53540174823413E-14,0.));
#12407=DIRECTION('',(0.,0.,1.));
#12408=DIRECTION('center_axis',(0.,0.,-1.));
#12409=DIRECTION('ref_axis',(1.,0.,0.));
#12410=DIRECTION('center_axis',(0.,0.,-1.));
#12411=DIRECTION('ref_axis',(1.,0.,0.));
#12412=DIRECTION('',(0.707106781186548,8.65956056235493E-17,0.707106781186547));
#12413=DIRECTION('center_axis',(0.,0.,1.));
#12414=DIRECTION('ref_axis',(1.,0.,0.));
#12415=DIRECTION('center_axis',(0.,0.,1.));
#12416=DIRECTION('ref_axis',(1.,7.53540174823413E-14,0.));
#12417=DIRECTION('center_axis',(0.,0.,-1.));
#12418=DIRECTION('ref_axis',(1.,7.53540174823413E-14,0.));
#12419=DIRECTION('center_axis',(0.,0.,1.));
#12420=DIRECTION('ref_axis',(1.,0.,0.));
#12421=DIRECTION('center_axis',(-2.40370335797945E-16,-1.,0.));
#12422=DIRECTION('ref_axis',(1.,-2.40370335797945E-16,0.));
#12423=DIRECTION('',(1.,-2.40370335797945E-16,0.));
#12424=DIRECTION('',(0.,0.,1.));
#12425=DIRECTION('',(1.,-2.40370335797945E-16,0.));
#12426=DIRECTION('',(0.,0.,1.));
#12427=DIRECTION('center_axis',(-0.866025403784439,-0.5,0.));
#12428=DIRECTION('ref_axis',(0.5,-0.866025403784439,0.));
#12429=DIRECTION('',(0.5,-0.866025403784439,0.));
#12430=DIRECTION('',(0.,0.,1.));
#12431=DIRECTION('',(0.5,-0.866025403784439,0.));
#12432=DIRECTION('center_axis',(-0.866025403784439,0.5,0.));
#12433=DIRECTION('ref_axis',(-0.5,-0.866025403784439,0.));
#12434=DIRECTION('',(-0.5,-0.866025403784439,0.));
#12435=DIRECTION('',(0.,0.,1.));
#12436=DIRECTION('',(-0.5,-0.866025403784439,0.));
#12437=DIRECTION('center_axis',(1.20185167898973E-16,1.,0.));
#12438=DIRECTION('ref_axis',(-1.,1.20185167898973E-16,0.));
#12439=DIRECTION('',(-1.,1.20185167898973E-16,0.));
#12440=DIRECTION('',(0.,0.,1.));
#12441=DIRECTION('',(-1.,1.20185167898973E-16,0.));
#12442=DIRECTION('center_axis',(0.866025403784439,0.5,0.));
#12443=DIRECTION('ref_axis',(-0.5,0.866025403784439,0.));
#12444=DIRECTION('',(-0.5,0.866025403784439,0.));
#12445=DIRECTION('',(0.,0.,1.));
#12446=DIRECTION('',(-0.5,0.866025403784439,0.));
#12447=DIRECTION('center_axis',(0.866025403784439,-0.5,0.));
#12448=DIRECTION('ref_axis',(0.5,0.866025403784439,0.));
#12449=DIRECTION('',(0.5,0.866025403784439,0.));
#12450=DIRECTION('',(0.5,0.866025403784439,0.));
#12451=DIRECTION('center_axis',(0.,0.,1.));
#12452=DIRECTION('ref_axis',(1.,0.,0.));
#12453=DIRECTION('center_axis',(0.,0.,1.));
#12454=DIRECTION('ref_axis',(1.,0.,0.));
#12455=DIRECTION('center_axis',(0.,0.,1.));
#12456=DIRECTION('ref_axis',(1.,0.,0.));
#12457=DIRECTION('center_axis',(0.,0.,1.));
#12458=DIRECTION('ref_axis',(1.,0.,0.));
#12459=DIRECTION('',(0.,0.,-1.));
#12460=DIRECTION('center_axis',(0.,0.,1.));
#12461=DIRECTION('ref_axis',(1.,0.,0.));
#12462=DIRECTION('center_axis',(0.,0.,1.));
#12463=DIRECTION('ref_axis',(1.,0.,0.));
#12464=DIRECTION('center_axis',(0.,0.,1.));
#12465=DIRECTION('ref_axis',(1.,0.,0.));
#32053=CARTESIAN_POINT('',(0.,0.,0.));
#32054=CARTESIAN_POINT('Origin',(0.,0.,0.));
#32055=CARTESIAN_POINT('',(-0.146530139441781,9.2983754875535E-5,0.0160655045842905));
#32056=CARTESIAN_POINT('',(-0.146482381647069,0.000161727750000726,0.00893449541570906));
#32057=CARTESIAN_POINT('',(-0.14635,-1.79227059055215E-17,0.));
#32058=CARTESIAN_POINT('',(0.0634007094575212,0.131904027763685,0.));
#32059=CARTESIAN_POINT('Ctrl Pts',(-0.146530139441781,9.2983754875535E-5,
0.0160655045842905));
#32060=CARTESIAN_POINT('Ctrl Pts',(-0.146562770122328,0.00491041321584185,
0.015802617364053));
#32061=CARTESIAN_POINT('Ctrl Pts',(-0.146345876989778,0.00972466734833348,
0.0155397301438155));
#32062=CARTESIAN_POINT('Ctrl Pts',(-0.145869825450435,0.0145129075872385,
0.015276842923578));
#32063=CARTESIAN_POINT('Ctrl Pts',(-0.141074879536054,0.0627416203906926,
0.0126289573514387));
#32064=CARTESIAN_POINT('Ctrl Pts',(-0.109987863649871,0.10833117855941,
0.00998107177929941));
#32065=CARTESIAN_POINT('Ctrl Pts',(-0.0668435938445389,0.130448755664999,
0.00733318620716011));
#32066=CARTESIAN_POINT('Ctrl Pts',(-0.0270149638383408,0.150866595604039,
0.00488879080477341));
#32067=CARTESIAN_POINT('Ctrl Pts',(0.0230889279919825,0.151281476944728,
0.00244439540238672));
#32068=CARTESIAN_POINT('Ctrl Pts',(0.0635548502597316,0.132093933345895,
1.98375346423187E-17));
#32069=CARTESIAN_POINT('',(-0.0634007094575231,0.131904027763684,0.));
#32070=CARTESIAN_POINT('Origin',(0.,0.,0.));
#32071=CARTESIAN_POINT('Ctrl Pts',(-0.063400709457523,0.131904027763684,
7.63278329429795E-17));
#32072=CARTESIAN_POINT('Ctrl Pts',(-0.107339749959442,0.110784382003545,
0.00265083470503432));
#32073=CARTESIAN_POINT('Ctrl Pts',(-0.139511904869873,0.0661645412785542,
0.00530166941006857));
#32074=CARTESIAN_POINT('Ctrl Pts',(-0.145460797893518,0.0180856147189845,
0.00795250411510281));
#32075=CARTESIAN_POINT('Ctrl Pts',(-0.146195379242097,0.0121487315761866,
0.00827983454863823));
#32076=CARTESIAN_POINT('Ctrl Pts',(-0.146530113272026,0.00615910494930538,
0.00860716498217364));
#32077=CARTESIAN_POINT('Ctrl Pts',(-0.146482381647069,0.000161727750000726,
0.00893449541570906));
#32078=CARTESIAN_POINT('Origin',(0.,0.,0.));
#32079=CARTESIAN_POINT('',(-0.146153148300412,8.02585168747302E-5,0.0660655045842906));
#32080=CARTESIAN_POINT('',(-0.146138869890956,7.0051777900314E-5,0.058934495415709));
#32081=CARTESIAN_POINT('',(-0.14635,-1.79227059055215E-17,0.));
#32082=CARTESIAN_POINT('Ctrl Pts',(-0.146153148300412,8.02585168747302E-5,
0.0660655045842906));
#32083=CARTESIAN_POINT('Ctrl Pts',(-0.146248563607689,0.0193075654691076,
0.0650232641302222));
#32084=CARTESIAN_POINT('Ctrl Pts',(-0.142725320554989,0.0385012587497889,
0.0639810236761539));
#32085=CARTESIAN_POINT('Ctrl Pts',(-0.135419901199499,0.0561272788093185,
0.0629387832220855));
#32086=CARTESIAN_POINT('Ctrl Pts',(-0.116859966748363,0.100907429136131,
0.0602908976499462));
#32087=CARTESIAN_POINT('Ctrl Pts',(-0.0738879770866151,0.13556903337647,
0.0576430120778069));
#32088=CARTESIAN_POINT('Ctrl Pts',(-0.0261938646990992,0.144231038496032,
0.0549951265056676));
#32089=CARTESIAN_POINT('Ctrl Pts',(0.0215002476884163,0.152893043615593,
0.0523472409335283));
#32090=CARTESIAN_POINT('Ctrl Pts',(0.0739164828016995,0.135555449614377,
0.049699355361389));
#32091=CARTESIAN_POINT('Ctrl Pts',(0.107036887564708,0.100160226311824,
0.0470514697892497));
#32092=CARTESIAN_POINT('Ctrl Pts',(0.140157292327717,0.0647650030092702,
0.0444035842171104));
#32093=CARTESIAN_POINT('Ctrl Pts',(0.153981866740452,0.0113121504053791,
0.0417556986449711));
#32094=CARTESIAN_POINT('Ctrl Pts',(0.142176802105062,-0.0357014716925755,
0.0391078130728318));
#32095=CARTESIAN_POINT('Ctrl Pts',(0.130371737469673,-0.0827150937905301,
0.0364599275006924));
#32096=CARTESIAN_POINT('Ctrl Pts',(0.0929370337861598,-0.123289485382548,
0.0338120419285532));
#32097=CARTESIAN_POINT('Ctrl Pts',(0.047024206385633,-0.138841291698229,
0.0311641563564138));
#32098=CARTESIAN_POINT('Ctrl Pts',(0.0011113789851062,-0.15439309801391,
0.0285162707842745));
#32099=CARTESIAN_POINT('Ctrl Pts',(-0.0532795721324345,-0.144922319053254,
0.0258683852121352));
#32100=CARTESIAN_POINT('Ctrl Pts',(-0.091223609719915,-0.11475299585383,
0.0232204996399959));
#32101=CARTESIAN_POINT('Ctrl Pts',(-0.125400489590719,-0.0875789416327165,
0.0208355012880941));
#32102=CARTESIAN_POINT('Ctrl Pts',(-0.146234103296486,-0.0436123029244358,
0.0184505029361923));
#32103=CARTESIAN_POINT('Ctrl Pts',(-0.146530139441781,9.2983754875535E-5,
0.0160655045842905));
#32104=CARTESIAN_POINT('Ctrl Pts',(-0.146482381647069,0.000161727750000726,
0.00893449541570906));
#32105=CARTESIAN_POINT('Ctrl Pts',(-0.146143566116611,-0.0424097233364945,
0.0112579996872079));
#32106=CARTESIAN_POINT('Ctrl Pts',(-0.126533645440834,-0.0853716986287587,
0.0135815039587068));
#32107=CARTESIAN_POINT('Ctrl Pts',(-0.0938693583126354,-0.112632000129883,
0.0159050082302056));
#32108=CARTESIAN_POINT('Ctrl Pts',(-0.0566033945712489,-0.143732676025031,
0.0185558429352399));
#32109=CARTESIAN_POINT('Ctrl Pts',(-0.00234583595161722,-0.154396015421179,
0.0212066776402742));
#32110=CARTESIAN_POINT('Ctrl Pts',(0.0439541262059228,-0.139833200290426,
0.0238575123453084));
#32111=CARTESIAN_POINT('Ctrl Pts',(0.0902540883634627,-0.125270385159674,
0.0265083470503427));
#32112=CARTESIAN_POINT('Ctrl Pts',(0.128596454058911,-0.0854814155020214,
0.029159181755377));
#32113=CARTESIAN_POINT('Ctrl Pts',(0.141395806078876,-0.0386806767328055,
0.0318100164604112));
#32114=CARTESIAN_POINT('Ctrl Pts',(0.154195158098842,0.00812006203641059,
0.0344608511654455));
#32115=CARTESIAN_POINT('Ctrl Pts',(0.141451496443324,0.0619325699171903,
0.0371116858704798));
#32116=CARTESIAN_POINT('Ctrl Pts',(0.109005912554766,0.0980207644158424,
0.0397625205755141));
#32117=CARTESIAN_POINT('Ctrl Pts',(0.0765603286662091,0.134108958914494,
0.0424133552805484));
#32118=CARTESIAN_POINT('Ctrl Pts',(0.0244128225446121,0.152472840031019,
0.0450641899855826));
#32119=CARTESIAN_POINT('Ctrl Pts',(-0.0234881253671046,0.144695681732891,
0.0477150246906169));
#32120=CARTESIAN_POINT('Ctrl Pts',(-0.0713890732788212,0.136918523434763,
0.0503658593956511));
#32121=CARTESIAN_POINT('Ctrl Pts',(-0.115043462980658,0.103000325721984,
0.0530166941006854));
#32122=CARTESIAN_POINT('Ctrl Pts',(-0.134410456092164,0.0585065536587812,
0.0556675288057197));
#32123=CARTESIAN_POINT('Ctrl Pts',(-0.142366606622288,0.0402280761403725,
0.0567565176757161));
#32124=CARTESIAN_POINT('Ctrl Pts',(-0.14622390219053,0.0201648150927879,
0.0578455065457126));
#32125=CARTESIAN_POINT('Ctrl Pts',(-0.146138869890956,7.0051777900314E-5,
0.058934495415709));
#32126=CARTESIAN_POINT('Origin',(0.,0.,0.));
#32127=CARTESIAN_POINT('',(-0.146239229308481,-0.000121680145597616,0.116065504584291));
#32128=CARTESIAN_POINT('',(-0.146251911109041,-0.00012571917928438,0.108934495415709));
#32129=CARTESIAN_POINT('',(-0.14635,-1.79227059055215E-17,0.));
#32130=CARTESIAN_POINT('Ctrl Pts',(-0.146239229308481,-0.000121680145597616,
0.116065504584291));
#32131=CARTESIAN_POINT('Ctrl Pts',(-0.145975985392548,0.0334333989639988,
0.114243910896391));
#32132=CARTESIAN_POINT('Ctrl Pts',(-0.134505001919181,0.0671510842014817,
0.112422317208492));
#32133=CARTESIAN_POINT('Ctrl Pts',(-0.113362446108109,0.09293957845923,
0.110600723520593));
#32134=CARTESIAN_POINT('Ctrl Pts',(-0.0826294298146382,0.130425974204838,
0.107952837948454));
#32135=CARTESIAN_POINT('Ctrl Pts',(-0.0314605739124977,0.151158147427946,
0.105304952376314));
#32136=CARTESIAN_POINT('Ctrl Pts',(0.0166981167953111,0.145636463652384,
0.102657066804175));
#32137=CARTESIAN_POINT('Ctrl Pts',(0.0648568075031199,0.140114779876822,
0.100009181232036));
#32138=CARTESIAN_POINT('Ctrl Pts',(0.110005333016597,0.10833923910259,0.0973612956598965));
#32139=CARTESIAN_POINT('Ctrl Pts',(0.1314562431614,0.0648696188566969,0.0947134100877572));
#32140=CARTESIAN_POINT('Ctrl Pts',(0.152907153306203,0.0213999986108032,
0.0920655245156179));
#32141=CARTESIAN_POINT('Ctrl Pts',(0.150660448082332,-0.0337637011067522,
0.0894176389434786));
#32142=CARTESIAN_POINT('Ctrl Pts',(0.125745602608234,-0.075344908113871,
0.0867697533713393));
#32143=CARTESIAN_POINT('Ctrl Pts',(0.100830757134136,-0.11692611512099,
0.0841218677992));
#32144=CARTESIAN_POINT('Ctrl Pts',(0.053247771409812,-0.144924829417672,
0.0814739822270607));
#32145=CARTESIAN_POINT('Ctrl Pts',(0.00479954857812182,-0.146511973337632,
0.0788260966549214));
#32146=CARTESIAN_POINT('Ctrl Pts',(-0.0436486742535683,-0.148099117257592,
0.0761782110827821));
#32147=CARTESIAN_POINT('Ctrl Pts',(-0.0929621341926243,-0.123274690800829,
0.0735303255106428));
#32148=CARTESIAN_POINT('Ctrl Pts',(-0.120544924541891,-0.0834131293658051,
0.0708824399385034));
#32149=CARTESIAN_POINT('Ctrl Pts',(-0.137270788050899,-0.059241570673742,
0.0692767948204325));
#32150=CARTESIAN_POINT('Ctrl Pts',(-0.146006154272575,-0.0295407674383123,
0.0676711497023615));
#32151=CARTESIAN_POINT('Ctrl Pts',(-0.146153148300412,8.02585168747302E-5,
0.0660655045842906));
#32152=CARTESIAN_POINT('Ctrl Pts',(-0.146138869890956,7.0051777900314E-5,
0.058934495415709));
#32153=CARTESIAN_POINT('Ctrl Pts',(-0.14601691516158,-0.0287501898739087,
0.0604963412507468));
#32154=CARTESIAN_POINT('Ctrl Pts',(-0.137785682499354,-0.0576352309664648,
0.0620581870857847));
#32155=CARTESIAN_POINT('Ctrl Pts',(-0.121906950385236,-0.0814126279516829,
0.0636200329208225));
#32156=CARTESIAN_POINT('Ctrl Pts',(-0.0949568550456235,-0.121768691085319,
0.0662708676258568));
#32157=CARTESIAN_POINT('Ctrl Pts',(-0.0459770678452217,-0.147411470938967,
0.068921702330891));
#32158=CARTESIAN_POINT('Ctrl Pts',(0.00254289383979588,-0.146569427669784,
0.0715725370359253));
#32159=CARTESIAN_POINT('Ctrl Pts',(0.0510628555248136,-0.145727384400601,
0.0742233717409596));
#32160=CARTESIAN_POINT('Ctrl Pts',(0.0991229916944473,-0.118400518008588,
0.0768742064459939));
#32161=CARTESIAN_POINT('Ctrl Pts',(0.124657213858417,-0.0771346353870958,
0.0795250411510281));
#32162=CARTESIAN_POINT('Ctrl Pts',(0.150191436022387,-0.0358687527656039,
0.0821758758560624));
#32163=CARTESIAN_POINT('Ctrl Pts',(0.153199744180694,0.0193361460853669,
0.0848267105610966));
#32164=CARTESIAN_POINT('Ctrl Pts',(0.132300679968259,0.0631324945868766,
0.0874775452661308));
#32165=CARTESIAN_POINT('Ctrl Pts',(0.111401615755824,0.106928843088387,
0.0901283799711651));
#32166=CARTESIAN_POINT('Ctrl Pts',(0.0665951791726482,0.139316641240435,
0.0927792146761994));
#32167=CARTESIAN_POINT('Ctrl Pts',(0.0184540622028837,0.145425561817519,
0.0954300493812337));
#32168=CARTESIAN_POINT('Ctrl Pts',(-0.0296870547668806,0.151534482394603,
0.098080884086268));
#32169=CARTESIAN_POINT('Ctrl Pts',(-0.0811628521232332,0.131364525396722,
0.100731718791302));
#32170=CARTESIAN_POINT('Ctrl Pts',(-0.11233861635763,0.0941764269143644,
0.103382553496337));
#32171=CARTESIAN_POINT('Ctrl Pts',(-0.134103588725605,0.0682140181085839,
0.105233200802794));
#32172=CARTESIAN_POINT('Ctrl Pts',(-0.145974404722175,0.0339570340187871,
0.107083848109252));
#32173=CARTESIAN_POINT('Ctrl Pts',(-0.146251911109041,-0.00012571917928438,
0.108934495415709));
#32174=CARTESIAN_POINT('Origin',(0.,0.,0.));
#32175=CARTESIAN_POINT('',(-0.146588437557148,-1.60561805771647E-5,0.166065504584291));
#32176=CARTESIAN_POINT('',(-0.146590338660816,-1.32548991986104E-5,0.158934495415709));
#32177=CARTESIAN_POINT('',(-0.14635,-1.79227059055215E-17,0.));
#32178=CARTESIAN_POINT('Ctrl Pts',(-0.146588437557148,-1.60561805771647E-5,
0.166065504584291));
#32179=CARTESIAN_POINT('Ctrl Pts',(-0.146514434076835,0.0476007616257437,
0.163464557662561));
#32180=CARTESIAN_POINT('Ctrl Pts',(-0.121147481081461,0.0952852365283555,
0.160863610740831));
#32181=CARTESIAN_POINT('Ctrl Pts',(-0.0815892695913163,0.121786698620987,
0.158262663819101));
#32182=CARTESIAN_POINT('Ctrl Pts',(-0.0413171607723027,0.148766426092319,
0.155614778246961));
#32183=CARTESIAN_POINT('Ctrl Pts',(0.0136630407409267,0.153791672495834,
0.152966892674822));
#32184=CARTESIAN_POINT('Ctrl Pts',(0.0581589346640781,0.134559827321239,
0.150319007102683));
#32185=CARTESIAN_POINT('Ctrl Pts',(0.10265482858723,0.115327982146644,0.147671121530543));
#32186=CARTESIAN_POINT('Ctrl Pts',(0.136666414920303,0.0718390453939375,
0.145023235958404));
#32187=CARTESIAN_POINT('Ctrl Pts',(0.144609292620067,0.0240200202446034,
0.142375350386265));
#32188=CARTESIAN_POINT('Ctrl Pts',(0.152552170319831,-0.0237990049047303,
0.139727464814125));
#32189=CARTESIAN_POINT('Ctrl Pts',(0.134426339386286,-0.0759481184506919,
0.137079579241986));
#32190=CARTESIAN_POINT('Ctrl Pts',(0.0985372115045479,-0.108532146892156,
0.134431693669847));
#32191=CARTESIAN_POINT('Ctrl Pts',(0.06264808362281,-0.141116175333621,
0.131783808097708));
#32192=CARTESIAN_POINT('Ctrl Pts',(0.00899565879287956,-0.154135118670589,
0.129135922525568));
#32193=CARTESIAN_POINT('Ctrl Pts',(-0.0378360619111076,-0.141623588974912,
0.126488036953429));
#32194=CARTESIAN_POINT('Ctrl Pts',(-0.0846677826150948,-0.129112059279235,
0.12384015138129));
#32195=CARTESIAN_POINT('Ctrl Pts',(-0.124678799193139,-0.0910700565509135,
0.12119226580915));
#32196=CARTESIAN_POINT('Ctrl Pts',(-0.13953571913976,-0.0449287460526992,
0.118544380237011));
#32197=CARTESIAN_POINT('Ctrl Pts',(-0.144171928689699,-0.0305300156868414,
0.117718088352771));
#32198=CARTESIAN_POINT('Ctrl Pts',(-0.146358639203649,-0.0153425769501271,
0.116891796468531));
#32199=CARTESIAN_POINT('Ctrl Pts',(-0.146239229308481,-0.000121680145597616,
0.116065504584291));
#32200=CARTESIAN_POINT('Ctrl Pts',(-0.146251911109041,-0.00012571917928438,
0.108934495415709));
#32201=CARTESIAN_POINT('Ctrl Pts',(-0.146371899997805,-0.01486250318061,
0.109734682814286));
#32202=CARTESIAN_POINT('Ctrl Pts',(-0.144324466618943,-0.0295667139196708,
0.110534870212863));
#32203=CARTESIAN_POINT('Ctrl Pts',(-0.139972258433256,-0.0435537680369422,
0.111335057611439));
#32204=CARTESIAN_POINT('Ctrl Pts',(-0.125554405162046,-0.0898896245390587,
0.113985892316474));
#32205=CARTESIAN_POINT('Ctrl Pts',(-0.0858429675071836,-0.128355097576459,
0.116636727021508));
#32206=CARTESIAN_POINT('Ctrl Pts',(-0.0390712063381835,-0.141289065177804,
0.119287561726542));
#32207=CARTESIAN_POINT('Ctrl Pts',(0.00770055483081633,-0.15422303277915,
0.121938396431576));
#32208=CARTESIAN_POINT('Ctrl Pts',(0.061532639513954,-0.141625494944442,
0.124589231136611));
#32209=CARTESIAN_POINT('Ctrl Pts',(0.0977084099269336,-0.109280503770194,
0.127240065841645));
#32210=CARTESIAN_POINT('Ctrl Pts',(0.133884180339913,-0.0769355125959451,
0.129890900546679));
#32211=CARTESIAN_POINT('Ctrl Pts',(0.152403636482735,-0.024843068082156,
0.132541735251714));
#32212=CARTESIAN_POINT('Ctrl Pts',(0.144763687764892,0.0230789149168219,
0.135192569956748));
#32213=CARTESIAN_POINT('Ctrl Pts',(0.137123739047049,0.0710008979157997,
0.137843404661782));
#32214=CARTESIAN_POINT('Ctrl Pts',(0.103324385468542,0.114752419399967,
0.140494239366816));
#32215=CARTESIAN_POINT('Ctrl Pts',(0.058884379534592,0.134245263752326,
0.143145074071851));
#32216=CARTESIAN_POINT('Ctrl Pts',(0.0144443736006417,0.153738108104685,
0.145795908776885));
#32217=CARTESIAN_POINT('Ctrl Pts',(-0.0406362846887521,0.148972275325237,
0.148446743481919));
#32218=CARTESIAN_POINT('Ctrl Pts',(-0.0810676758629916,0.122135962547369,
0.151097578186953));
#32219=CARTESIAN_POINT('Ctrl Pts',(-0.120911410803562,0.0956897062586433,
0.153709883929872));
#32220=CARTESIAN_POINT('Ctrl Pts',(-0.146528627904579,0.0478098809758598,
0.15632218967279));
#32221=CARTESIAN_POINT('Ctrl Pts',(-0.146590338660816,-1.32548991986104E-5,
0.158934495415709));
#32222=CARTESIAN_POINT('Origin',(0.,0.,0.));
#32223=CARTESIAN_POINT('',(-0.146286659309134,0.000131086592791319,0.21606550458429));
#32224=CARTESIAN_POINT('',(-0.146291727422766,0.000132510687651112,0.208934495415709));
#32225=CARTESIAN_POINT('',(-0.14635,-1.79227059055215E-17,0.));
#32226=CARTESIAN_POINT('Ctrl Pts',(-0.146286659309134,0.000131086592791319,
0.21606550458429));
#32227=CARTESIAN_POINT('Ctrl Pts',(-0.146403448836959,0.0136116234039521,
0.215333090000869));
#32228=CARTESIAN_POINT('Ctrl Pts',(-0.144693388849564,0.0270630787330369,
0.214600675417447));
#32229=CARTESIAN_POINT('Ctrl Pts',(-0.141038079685752,0.0399633448807191,
0.213868260834026));
#32230=CARTESIAN_POINT('Ctrl Pts',(-0.127823104703478,0.0866014503777888,
0.211220375261887));
#32231=CARTESIAN_POINT('Ctrl Pts',(-0.0891832035626152,0.126035366094718,
0.208572489689747));
#32232=CARTESIAN_POINT('Ctrl Pts',(-0.0428235107164534,0.140196133277333,
0.205924604117608));
#32233=CARTESIAN_POINT('Ctrl Pts',(0.00353618212970767,0.154356900459949,
0.203276718545469));
#32234=CARTESIAN_POINT('Ctrl Pts',(0.0576156666811676,0.143244519108251,
0.200628832973329));
#32235=CARTESIAN_POINT('Ctrl Pts',(0.0946352588096336,0.111950777776248,
0.19798094740119));
#32236=CARTESIAN_POINT('Ctrl Pts',(0.1316548509381,0.0806570364442455,0.195333061829051));
#32237=CARTESIAN_POINT('Ctrl Pts',(0.151614550643572,0.0291819351319375,
0.192685176256911));
#32238=CARTESIAN_POINT('Ctrl Pts',(0.145368652149886,-0.0188881928126718,
0.190037290684772));
#32239=CARTESIAN_POINT('Ctrl Pts',(0.1391227536562,-0.0669583207572802,
0.187389405112633));
#32240=CARTESIAN_POINT('Ctrl Pts',(0.106671256963357,-0.11162347533419,
0.184741519540494));
#32241=CARTESIAN_POINT('Ctrl Pts',(0.06288371648092,-0.132417699194711,
0.182093633968354));
#32242=CARTESIAN_POINT('Ctrl Pts',(0.0190961759984827,-0.153211923055232,
0.179445748396215));
#32243=CARTESIAN_POINT('Ctrl Pts',(-0.0360274082735484,-0.150135216199364,
0.176797862824076));
#32244=CARTESIAN_POINT('Ctrl Pts',(-0.0772289367619549,-0.124597352202288,
0.174149977251936));
#32245=CARTESIAN_POINT('Ctrl Pts',(-0.118430465250361,-0.0990594882052125,
0.171502091679797));
#32246=CARTESIAN_POINT('Ctrl Pts',(-0.145709937955143,-0.0510604670669293,
0.168854206107658));
#32247=CARTESIAN_POINT('Ctrl Pts',(-0.146567666245136,-0.00259385222821292,
0.166206320535519));
#32248=CARTESIAN_POINT('Ctrl Pts',(-0.146582871059412,-0.00173469218203314,
0.166159381885109));
#32249=CARTESIAN_POINT('Ctrl Pts',(-0.146589773079785,-0.000875385198767554,
0.1661124432347));
#32250=CARTESIAN_POINT('Ctrl Pts',(-0.146588437557148,-1.60561805771647E-5,
0.166065504584291));
#32251=CARTESIAN_POINT('Ctrl Pts',(-0.146590338660816,-1.32548991986104E-5,
0.158934495415709));
#32252=CARTESIAN_POINT('Ctrl Pts',(-0.146591248834288,-0.000718599514920206,
0.158973024377825));
#32253=CARTESIAN_POINT('Ctrl Pts',(-0.146586599823099,-0.0014239317987834,
0.15901155333994));
#32254=CARTESIAN_POINT('Ctrl Pts',(-0.146576355279203,-0.00212918280121965,
0.159050082302056));
#32255=CARTESIAN_POINT('Ctrl Pts',(-0.14587151946209,-0.0506512225956504,
0.16170091700709));
#32256=CARTESIAN_POINT('Ctrl Pts',(-0.118679723768778,-0.0987885094082227,
0.164351751712125));
#32257=CARTESIAN_POINT('Ctrl Pts',(-0.0774859020747837,-0.12443912668017,
0.167002586417159));
#32258=CARTESIAN_POINT('Ctrl Pts',(-0.0362920803807891,-0.150089743952118,
0.169653421122193));
#32259=CARTESIAN_POINT('Ctrl Pts',(0.0189037673138887,-0.153253691683441,
0.172304255827227));
#32260=CARTESIAN_POINT('Ctrl Pts',(0.0627588320121262,-0.132478263640569,
0.174955090532262));
#32261=CARTESIAN_POINT('Ctrl Pts',(0.106613896710364,-0.111702835597697,
0.177605925237296));
#32262=CARTESIAN_POINT('Ctrl Pts',(0.139128178412161,-0.0669880317806311,
0.18025675994233));
#32263=CARTESIAN_POINT('Ctrl Pts',(0.14537295917033,-0.0188643595177345,
0.182907594647365));
#32264=CARTESIAN_POINT('Ctrl Pts',(0.151617739928498,0.0292593127451622,
0.185558429352399));
#32265=CARTESIAN_POINT('Ctrl Pts',(0.131593019743037,0.0807918534538889,
0.188209264057433));
#32266=CARTESIAN_POINT('Ctrl Pts',(0.0944930167757219,0.11207243679613,
0.190860098762467));
#32267=CARTESIAN_POINT('Ctrl Pts',(0.0573930138084077,0.143353020138371,
0.193510933467502));
#32268=CARTESIAN_POINT('Ctrl Pts',(0.00321772805924021,0.154381646114126,
0.196161768172536));
#32269=CARTESIAN_POINT('Ctrl Pts',(-0.0431586156002514,0.14009459381994,
0.19881260287757));
#32270=CARTESIAN_POINT('Ctrl Pts',(-0.0895349592597434,0.125807541525753,
0.201463437582605));
#32271=CARTESIAN_POINT('Ctrl Pts',(-0.12811236082956,0.086204810961624,
0.204114272287639));
#32272=CARTESIAN_POINT('Ctrl Pts',(-0.141178260973432,0.0394697345298879,
0.206765106992673));
#32273=CARTESIAN_POINT('Ctrl Pts',(-0.144742548661738,0.0267207271363346,
0.207488236467018));
#32274=CARTESIAN_POINT('Ctrl Pts',(-0.146408370233879,0.0134409584703521,
0.208211365941364));
#32275=CARTESIAN_POINT('Ctrl Pts',(-0.146291727422766,0.000132510687651112,
0.208934495415709));
#32276=CARTESIAN_POINT('Origin',(0.,0.,0.));
#32277=CARTESIAN_POINT('',(-0.146128981728208,-5.54263297282837E-5,0.26606550458429));
#32278=CARTESIAN_POINT('',(-0.146122305401386,-4.76483376818115E-5,0.258934495415709));
#32279=CARTESIAN_POINT('',(-0.14635,-1.79227059055215E-17,0.));
#32280=CARTESIAN_POINT('Ctrl Pts',(-0.146128981728208,-5.54263297282837E-5,
0.26606550458429));
#32281=CARTESIAN_POINT('Ctrl Pts',(-0.146034100463789,0.0278452262029135,
0.264553736767038));
#32282=CARTESIAN_POINT('Ctrl Pts',(-0.138353701663978,0.055794258172635,
0.263041968949786));
#32283=CARTESIAN_POINT('Ctrl Pts',(-0.123420870545114,0.0790954965178402,
0.261530201132533));
#32284=CARTESIAN_POINT('Ctrl Pts',(-0.0972657774021095,0.119907989099794,
0.258882315560394));
#32285=CARTESIAN_POINT('Ctrl Pts',(-0.0488616113353708,0.146461941272529,
0.256234429988255));
#32286=CARTESIAN_POINT('Ctrl Pts',(-0.000387576818673938,0.146590104167151,
0.253586544416116));
#32287=CARTESIAN_POINT('Ctrl Pts',(0.0480864576980232,0.146718267061773,
0.250938658843976));
#32288=CARTESIAN_POINT('Ctrl Pts',(0.0966303606646785,0.120420640678281,
0.248290773271837));
#32289=CARTESIAN_POINT('Ctrl Pts',(0.123000898959779,0.0797470232084743,
0.245642887699697));
#32290=CARTESIAN_POINT('Ctrl Pts',(0.149371437254879,0.0390734057386676,
0.242995002127558));
#32291=CARTESIAN_POINT('Ctrl Pts',(0.153568610878424,-0.0159762028174541,
0.240347116555419));
#32292=CARTESIAN_POINT('Ctrl Pts',(0.133669238840564,-0.0601775991819374,
0.23769923098328));
#32293=CARTESIAN_POINT('Ctrl Pts',(0.113769866802704,-0.104378995546421,
0.235051345411141));
#32294=CARTESIAN_POINT('Ctrl Pts',(0.0697739491034383,-0.137732179719266,
0.232403459839001));
#32295=CARTESIAN_POINT('Ctrl Pts',(0.0218407929672104,-0.144954436352131,
0.229755574266862));
#32296=CARTESIAN_POINT('Ctrl Pts',(-0.0260923631690164,-0.152176692984997,
0.227107688694722));
#32297=CARTESIAN_POINT('Ctrl Pts',(-0.0779627577422058,-0.133268022077883,
0.224459803122583));
#32298=CARTESIAN_POINT('Ctrl Pts',(-0.110002930616958,-0.0968925389857218,
0.221811917550444));
#32299=CARTESIAN_POINT('Ctrl Pts',(-0.133180677518425,-0.0705786441192844,
0.219896446561726));
#32300=CARTESIAN_POINT('Ctrl Pts',(-0.145981221709449,-0.0351243244252332,
0.217980975573008));
#32301=CARTESIAN_POINT('Ctrl Pts',(-0.146286659309134,0.000131086592791319,
0.21606550458429));
#32302=CARTESIAN_POINT('Ctrl Pts',(-0.146291727422766,0.000132510687651112,
0.208934495415709));
#32303=CARTESIAN_POINT('Ctrl Pts',(-0.14598078316578,-0.035344904233501,
0.210862200646398));
#32304=CARTESIAN_POINT('Ctrl Pts',(-0.13300294931328,-0.0710261241835679,
0.212789905877087));
#32305=CARTESIAN_POINT('Ctrl Pts',(-0.109555772823034,-0.0973996609618648,
0.214717611107776));
#32306=CARTESIAN_POINT('Ctrl Pts',(-0.0773129858108336,-0.133666557722538,
0.21736844581281));
#32307=CARTESIAN_POINT('Ctrl Pts',(-0.0252730130685043,-0.152332928944543,
0.220019280517844));
#32308=CARTESIAN_POINT('Ctrl Pts',(0.0226703353838526,-0.144828233467297,
0.222670115222879));
#32309=CARTESIAN_POINT('Ctrl Pts',(0.0706136838362102,-0.137323537990051,
0.225320949927913));
#32310=CARTESIAN_POINT('Ctrl Pts',(0.114460407998596,-0.103647775813554,
0.227971784632947));
#32311=CARTESIAN_POINT('Ctrl Pts',(0.134078573855527,-0.0592629508888991,
0.230622619337982));
#32312=CARTESIAN_POINT('Ctrl Pts',(0.153696739712459,-0.014878125964245,
0.233273454043016));
#32313=CARTESIAN_POINT('Ctrl Pts',(0.149086347263938,0.0402157617085659,
0.23592428874805));
#32314=CARTESIAN_POINT('Ctrl Pts',(0.122364227775469,0.080722717223899,
0.238575123453084));
#32315=CARTESIAN_POINT('Ctrl Pts',(0.0956421082870006,0.121229672739232,
0.241225958158119));
#32316=CARTESIAN_POINT('Ctrl Pts',(0.0468082617585844,0.147149696097087,
0.243876792863153));
#32317=CARTESIAN_POINT('Ctrl Pts',(-0.00171557347725478,0.146581779641701,
0.246527627568187));
#32318=CARTESIAN_POINT('Ctrl Pts',(-0.050239408713094,0.146013863186315,
0.249178462273221));
#32319=CARTESIAN_POINT('Ctrl Pts',(-0.0984532326563563,0.118958006917689,
0.251829296978256));
#32320=CARTESIAN_POINT('Ctrl Pts',(-0.124219986251493,0.0778367286753789,
0.25448013168329));
#32321=CARTESIAN_POINT('Ctrl Pts',(-0.13865248336877,0.054803841451165,
0.255964919594096));
#32322=CARTESIAN_POINT('Ctrl Pts',(-0.146042539478052,0.0273581331787701,
0.257449707504903));
#32323=CARTESIAN_POINT('Ctrl Pts',(-0.146122305401386,-4.76483376818114E-5,
0.258934495415709));
#32324=CARTESIAN_POINT('Origin',(0.,0.,0.));
#32325=CARTESIAN_POINT('',(-0.146489966325848,-0.000104789085069334,0.31606550458429));
#32326=CARTESIAN_POINT('',(-0.146466968003471,-0.000114397412080779,0.308934495415709));
#32327=CARTESIAN_POINT('',(-0.14635,-1.79227059055215E-17,0.));
#32328=CARTESIAN_POINT('Ctrl Pts',(-0.146489966325848,-0.000104789085069334,
0.31606550458429));
#32329=CARTESIAN_POINT('Ctrl Pts',(-0.146149966214897,0.0419143941805715,
0.313774383533207));
#32330=CARTESIAN_POINT('Ctrl Pts',(-0.127114021003857,0.084202434124342,
0.311483262482124));
#32331=CARTESIAN_POINT('Ctrl Pts',(-0.09522591597141,0.111448794443947,
0.309192141431041));
#32332=CARTESIAN_POINT('Ctrl Pts',(-0.0583723183850411,0.142937852758646,
0.306544255858902));
#32333=CARTESIAN_POINT('Ctrl Pts',(-0.00435235065556675,0.154336043577878,
0.303896370286762));
#32334=CARTESIAN_POINT('Ctrl Pts',(0.0420815742217502,0.140420618022043,
0.301248484714623));
#32335=CARTESIAN_POINT('Ctrl Pts',(0.0885154990990669,0.126505192466209,
0.298600599142484));
#32336=CARTESIAN_POINT('Ctrl Pts',(0.127363381124227,0.0872761505353081,
0.295952713570344));
#32337=CARTESIAN_POINT('Ctrl Pts',(0.140824787209621,0.0407085760419468,
0.293304827998205));
#32338=CARTESIAN_POINT('Ctrl Pts',(0.154286193295015,-0.00585899845141487,
0.290656942426066));
#32339=CARTESIAN_POINT('Ctrl Pts',(0.142361123440642,-0.0597651055072374,
0.288009056853927));
#32340=CARTESIAN_POINT('Ctrl Pts',(0.110513747042986,-0.0963095040482439,
0.285361171281788));
#32341=CARTESIAN_POINT('Ctrl Pts',(0.07866637064533,-0.13285390258925,0.282713285709648));
#32342=CARTESIAN_POINT('Ctrl Pts',(0.0268966877043911,-0.152036592615441,
0.280065400137508));
#32343=CARTESIAN_POINT('Ctrl Pts',(-0.0210739885810971,-0.145067900862674,
0.277417514565369));
#32344=CARTESIAN_POINT('Ctrl Pts',(-0.0690446648665853,-0.138099209109907,
0.27476962899323));
#32345=CARTESIAN_POINT('Ctrl Pts',(-0.113216334496623,-0.104979135578184,
0.272121743421091));
#32346=CARTESIAN_POINT('Ctrl Pts',(-0.133349159202006,-0.0608835823167352,
0.269473857848951));
#32347=CARTESIAN_POINT('Ctrl Pts',(-0.141987470405663,-0.0419636782623391,
0.268337740094064));
#32348=CARTESIAN_POINT('Ctrl Pts',(-0.146200286519779,-0.0210232140769756,
0.267201622339177));
#32349=CARTESIAN_POINT('Ctrl Pts',(-0.146128981728208,-5.54263297282837E-5,
0.26606550458429));
#32350=CARTESIAN_POINT('Ctrl Pts',(-0.146122305401386,-4.76483376818114E-5,
0.258934495415709));
#32351=CARTESIAN_POINT('Ctrl Pts',(-0.146184947882857,-0.0215701994360498,
0.260100542209937));
#32352=CARTESIAN_POINT('Ctrl Pts',(-0.141739031650533,-0.0430681260504587,
0.261266589004165));
#32353=CARTESIAN_POINT('Ctrl Pts',(-0.132654825339554,-0.0623847627977247,
0.262432635798393));
#32354=CARTESIAN_POINT('Ctrl Pts',(-0.112003227585469,-0.106298275812525,
0.265083470503427));
#32355=CARTESIAN_POINT('Ctrl Pts',(-0.0673803488302883,-0.138938601626132,
0.267734305208461));
#32356=CARTESIAN_POINT('Ctrl Pts',(-0.019274489346019,-0.145319150065199,
0.270385139913496));
#32357=CARTESIAN_POINT('Ctrl Pts',(0.02883137013825,-0.151699698504265,
0.27303597461853));
#32358=CARTESIAN_POINT('Ctrl Pts',(0.0804202103516079,-0.131820469568792,
0.275686809323564));
#32359=CARTESIAN_POINT('Ctrl Pts',(0.11180535579315,-0.0948088800228575,
0.278337644028599));
#32360=CARTESIAN_POINT('Ctrl Pts',(0.143190501234693,-0.0577972904769225,
0.280988478733633));
#32361=CARTESIAN_POINT('Ctrl Pts',(0.154371951904419,-0.00365334032052542,
0.283639313438667));
#32362=CARTESIAN_POINT('Ctrl Pts',(0.14021581852446,0.0427631330787578,
0.286290148143701));
#32363=CARTESIAN_POINT('Ctrl Pts',(0.126059685144501,0.0891796064780407,
0.288940982848735));
#32364=CARTESIAN_POINT('Ctrl Pts',(0.0865659677148572,0.12786860312021,
0.29159181755377));
#32365=CARTESIAN_POINT('Ctrl Pts',(0.0398679459367864,0.141066325542232,
0.294242652258804));
#32366=CARTESIAN_POINT('Ctrl Pts',(-0.00683007584128473,0.154264047964254,
0.296893486963838));
#32367=CARTESIAN_POINT('Ctrl Pts',(-0.0607324019677826,0.141970496166129,
0.299544321668873));
#32368=CARTESIAN_POINT('Ctrl Pts',(-0.0970901351530201,0.109830173318867,
0.302195156373907));
#32369=CARTESIAN_POINT('Ctrl Pts',(-0.127901447813816,0.0825928994431667,
0.304441602721174));
#32370=CARTESIAN_POINT('Ctrl Pts',(-0.14611277332701,0.0411022848956265,
0.306688049068442));
#32371=CARTESIAN_POINT('Ctrl Pts',(-0.146466968003471,-0.000114397412080779,
0.308934495415709));
#32372=CARTESIAN_POINT('Origin',(0.,0.,0.));
#32373=CARTESIAN_POINT('',(-0.146456696168336,0.00011684297731019,0.36606550458429));
#32374=CARTESIAN_POINT('',(-0.146490622007778,0.000105425447882283,0.358934495415709));
#32375=CARTESIAN_POINT('',(-0.14635,-1.79227059055215E-17,0.));
#32376=CARTESIAN_POINT('Ctrl Pts',(-0.146456696168336,0.00011684297731019,
0.36606550458429));
#32377=CARTESIAN_POINT('Ctrl Pts',(-0.146524266643172,0.00787170677865199,
0.365642915871516));
#32378=CARTESIAN_POINT('Ctrl Pts',(-0.145961554618594,0.0156167466990778,
0.365220327158741));
#32379=CARTESIAN_POINT('Ctrl Pts',(-0.14473428578122,0.0232550097723626,
0.364797738445966));
#32380=CARTESIAN_POINT('Ctrl Pts',(-0.137044379852877,0.0711153666076302,
0.362149852873827));
#32381=CARTESIAN_POINT('Ctrl Pts',(-0.103263231798211,0.11478354525948,
0.359501967301688));
#32382=CARTESIAN_POINT('Ctrl Pts',(-0.0588696551343872,0.134250410014218,
0.356854081729549));
#32383=CARTESIAN_POINT('Ctrl Pts',(-0.0144760784705634,0.153717274768956,
0.354206196157409));
#32384=CARTESIAN_POINT('Ctrl Pts',(0.040529926802418,0.148982825626583,
0.35155831058527));
#32385=CARTESIAN_POINT('Ctrl Pts',(0.0809441375650951,0.122216428534895,
0.34891042501313));
#32386=CARTESIAN_POINT('Ctrl Pts',(0.121358348327771,0.0954500314432082,
0.346262539440991));
#32387=CARTESIAN_POINT('Ctrl Pts',(0.147180764580144,0.0466516864022081,
0.343614653868852));
#32388=CARTESIAN_POINT('Ctrl Pts',(0.146579333092572,-0.00181878629327471,
0.340966768296713));
#32389=CARTESIAN_POINT('Ctrl Pts',(0.145977901604999,-0.0502892589887582,
0.338318882724573));
#32390=CARTESIAN_POINT('Ctrl Pts',(0.11895262237748,-0.0984318593387246,
0.335670997152434));
#32391=CARTESIAN_POINT('Ctrl Pts',(0.0778867105927371,-0.124187234331756,
0.333023111580295));
#32392=CARTESIAN_POINT('Ctrl Pts',(0.036820798807994,-0.149942609324788,
0.330375226008155));
#32393=CARTESIAN_POINT('Ctrl Pts',(-0.0182857455339734,-0.153310758960884,
0.327727340436016));
#32394=CARTESIAN_POINT('Ctrl Pts',(-0.062182630799685,-0.132748368261283,
0.325079454863877));
#32395=CARTESIAN_POINT('Ctrl Pts',(-0.106079516065397,-0.112185977561681,
0.322431569291738));
#32396=CARTESIAN_POINT('Ctrl Pts',(-0.138766742254852,-0.0676930465263806,
0.319783683719598));
#32397=CARTESIAN_POINT('Ctrl Pts',(-0.145266741627948,-0.0196566181036479,
0.317135798147459));
#32398=CARTESIAN_POINT('Ctrl Pts',(-0.146142523114734,-0.0131843998326608,
0.316779033626403));
#32399=CARTESIAN_POINT('Ctrl Pts',(-0.14654290982994,-0.00664785401210523,
0.316422269105347));
#32400=CARTESIAN_POINT('Ctrl Pts',(-0.146489966325848,-0.000104789085069334,
0.31606550458429));
#32401=CARTESIAN_POINT('Ctrl Pts',(-0.146466968003471,-0.000114397412080779,
0.308934495415709));
#32402=CARTESIAN_POINT('Ctrl Pts',(-0.146530727462368,-0.00753391423752658,
0.309338883773476));
#32403=CARTESIAN_POINT('Ctrl Pts',(-0.146015835709215,-0.0149445544285316,
0.309743272131243));
#32404=CARTESIAN_POINT('Ctrl Pts',(-0.144891626709003,-0.0222615773186769,
0.31014766048901));
#32405=CARTESIAN_POINT('Ctrl Pts',(-0.137522244835771,-0.0702259112125575,
0.312798495194044));
#32406=CARTESIAN_POINT('Ctrl Pts',(-0.103970340845329,-0.114167485103918,
0.315449329899078));
#32407=CARTESIAN_POINT('Ctrl Pts',(-0.0596410500115333,-0.133910815353779,
0.318100164604112));
#32408=CARTESIAN_POINT('Ctrl Pts',(-0.015311759177738,-0.15365414560364,
0.320750999309147));
#32409=CARTESIAN_POINT('Ctrl Pts',(0.0397949184994109,-0.149199232212,0.323401834014181));
#32410=CARTESIAN_POINT('Ctrl Pts',(0.0803771156598139,-0.122591519257586,
0.326052668719215));
#32411=CARTESIAN_POINT('Ctrl Pts',(0.120959312820217,-0.0959838063031723,
0.32870350342425));
#32412=CARTESIAN_POINT('Ctrl Pts',(0.147017029463874,-0.0472232937859833,
0.331354338129284));
#32413=CARTESIAN_POINT('Ctrl Pts',(0.146586036983397,0.00130195078264539,
0.334005172834318));
#32414=CARTESIAN_POINT('Ctrl Pts',(0.146155044502921,0.0498271953512744,
0.336656007539352));
#32415=CARTESIAN_POINT('Ctrl Pts',(0.119235342898311,0.0981171719713431,
0.339306842244386));
#32416=CARTESIAN_POINT('Ctrl Pts',(0.0781869354735432,0.123999856599104,
0.341957676949421));
#32417=CARTESIAN_POINT('Ctrl Pts',(0.0371385280487761,0.149882541226865,
0.344608511654455));
#32418=CARTESIAN_POINT('Ctrl Pts',(-0.0180385851961482,0.153357933862318,
0.347259346359489));
#32419=CARTESIAN_POINT('Ctrl Pts',(-0.0620101968435835,0.132830330894432,
0.349910181064524));
#32420=CARTESIAN_POINT('Ctrl Pts',(-0.105981808491019,0.112302727926544,
0.352561015769558));
#32421=CARTESIAN_POINT('Ctrl Pts',(-0.138747918540966,0.0677721293553162,
0.355211850474592));
#32422=CARTESIAN_POINT('Ctrl Pts',(-0.145264183888347,0.0196844656531965,
0.357862685179626));
#32423=CARTESIAN_POINT('Ctrl Pts',(-0.146142422968675,0.0132033812753397,
0.358219955258321));
#32424=CARTESIAN_POINT('Ctrl Pts',(-0.146543841751789,0.00665768391130569,
0.358577225337015));
#32425=CARTESIAN_POINT('Ctrl Pts',(-0.146490622007778,0.000105425447882283,
0.358934495415709));
#32426=CARTESIAN_POINT('Origin',(0.,0.,0.));
#32427=CARTESIAN_POINT('',(-0.146117527463381,3.66422859593568E-5,0.416065504584291));
#32428=CARTESIAN_POINT('',(-0.146131941026353,6.08514395597815E-5,0.408934495415709));
#32429=CARTESIAN_POINT('',(-0.14635,-1.79227059055215E-17,0.));
#32430=CARTESIAN_POINT('Ctrl Pts',(-0.146117527463381,3.66422859593568E-5,
0.416065504584291));
#32431=CARTESIAN_POINT('Ctrl Pts',(-0.146167164015074,0.0222235765819606,
0.414863562637685));
#32432=CARTESIAN_POINT('Ctrl Pts',(-0.141430069804178,0.0443904018142415,
0.413661620691079));
#32433=CARTESIAN_POINT('Ctrl Pts',(-0.131797444393702,0.0641735569006793,
0.412459678744474));
#32434=CARTESIAN_POINT('Ctrl Pts',(-0.11057671079816,0.107755970404684,
0.409811793172335));
#32435=CARTESIAN_POINT('Ctrl Pts',(-0.0655968071821861,0.139769869286095,
0.407163907600195));
#32436=CARTESIAN_POINT('Ctrl Pts',(-0.0174679796227892,0.145546147336919,
0.404516022028056));
#32437=CARTESIAN_POINT('Ctrl Pts',(0.0306608479366084,0.151322425387742,
0.401868136455917));
#32438=CARTESIAN_POINT('Ctrl Pts',(0.0819385994394289,0.130861082607978,
0.399220250883777));
#32439=CARTESIAN_POINT('Ctrl Pts',(0.112869404704651,0.0935377150207321,
0.396572365311638));
#32440=CARTESIAN_POINT('Ctrl Pts',(0.143800209969873,0.0562143474334866,
0.393924479739499));
#32441=CARTESIAN_POINT('Ctrl Pts',(0.154384068997497,0.00202895503876042,
0.391276594167359));
#32442=CARTESIAN_POINT('Ctrl Pts',(0.139771347867625,-0.0441902675604103,
0.38862870859522));
#32443=CARTESIAN_POINT('Ctrl Pts',(0.125158626737753,-0.0904094901595803,
0.385980823023081));
#32444=CARTESIAN_POINT('Ctrl Pts',(0.0853493254503865,-0.128662542963195,
0.383332937450942));
#32445=CARTESIAN_POINT('Ctrl Pts',(0.0385844175605987,-0.141421539587247,
0.380685051878802));
#32446=CARTESIAN_POINT('Ctrl Pts',(-0.00818049032918902,-0.154180536211298,
0.378037166306663));
#32447=CARTESIAN_POINT('Ctrl Pts',(-0.0619010048213979,-0.141445476655787,
0.375389280734523));
#32448=CARTESIAN_POINT('Ctrl Pts',(-0.0979619301664915,-0.109051679368689,
0.372741395162384));
#32449=CARTESIAN_POINT('Ctrl Pts',(-0.128267720099621,-0.081827763001475,
0.370516098303019));
#32450=CARTESIAN_POINT('Ctrl Pts',(-0.146100878890467,-0.0407192549596569,
0.368290801443655));
#32451=CARTESIAN_POINT('Ctrl Pts',(-0.146456696168336,0.00011684297731019,
0.36606550458429));
#32452=CARTESIAN_POINT('Ctrl Pts',(-0.146490622007778,0.000105425447882283,
0.358934495415709));
#32453=CARTESIAN_POINT('Ctrl Pts',(-0.146148967529651,-0.0419580697355662,
0.361228060042049));
#32454=CARTESIAN_POINT('Ctrl Pts',(-0.12707053516474,-0.0842919640484707,
0.363521624668389));
#32455=CARTESIAN_POINT('Ctrl Pts',(-0.0951239884102214,-0.111537384525928,
0.365815189294729));
#32456=CARTESIAN_POINT('Ctrl Pts',(-0.0582011069398996,-0.143026842169921,
0.368466023999764));
#32457=CARTESIAN_POINT('Ctrl Pts',(-0.00408892335444046,-0.154361028624896,
0.371116858704798));
#32458=CARTESIAN_POINT('Ctrl Pts',(0.0423673101370894,-0.140335926848737,
0.373767693409832));
#32459=CARTESIAN_POINT('Ctrl Pts',(0.0888235436286192,-0.126310825072579,
0.376418528114866));
#32460=CARTESIAN_POINT('Ctrl Pts',(0.12762382702622,-0.0869264350652862,
0.379069362819901));
#32461=CARTESIAN_POINT('Ctrl Pts',(0.140953266768128,-0.0402658398230972,
0.381720197524935));
#32462=CARTESIAN_POINT('Ctrl Pts',(0.154282706510036,0.00639475541909176,
0.384371032229969));
#32463=CARTESIAN_POINT('Ctrl Pts',(0.142141302596253,0.0603315558961778,
0.387021866935004));
#32464=CARTESIAN_POINT('Ctrl Pts',(0.110103699587577,0.0967798361409283,
0.389672701640038));
#32465=CARTESIAN_POINT('Ctrl Pts',(0.0780660965789003,0.133228116385679,
0.392323536345072));
#32466=CARTESIAN_POINT('Ctrl Pts',(0.0261322944753315,0.152187876398094,
0.394974371050106));
#32467=CARTESIAN_POINT('Ctrl Pts',(-0.0218526425106493,0.144953866566232,
0.397625205755141));
#32468=CARTESIAN_POINT('Ctrl Pts',(-0.0698375794966294,0.13771985673437,
0.400276040460175));
#32469=CARTESIAN_POINT('Ctrl Pts',(-0.113873651365021,0.104292077058233,
0.402926875165209));
#32470=CARTESIAN_POINT('Ctrl Pts',(-0.133741989653421,0.0600186737328441,
0.405577709870243));
#32471=CARTESIAN_POINT('Ctrl Pts',(-0.142128499086628,0.0413306833614836,
0.406696638385399));
#32472=CARTESIAN_POINT('Ctrl Pts',(-0.14620899575881,0.0207103068323409,
0.407815566900554));
#32473=CARTESIAN_POINT('Ctrl Pts',(-0.146131941026353,6.08514395597814E-5,
0.408934495415709));
#32474=CARTESIAN_POINT('Origin',(0.,0.,0.));
#32475=CARTESIAN_POINT('',(-0.146320034481408,-0.000132042578932776,0.466065504584291));
#32476=CARTESIAN_POINT('',(-0.146267142220666,-0.000128791573925899,0.458934495415709));
#32477=CARTESIAN_POINT('',(-0.14635,-1.79227059055215E-17,0.));
#32478=CARTESIAN_POINT('Ctrl Pts',(-0.146320034481408,-0.000132042578932776,
0.466065504584291));
#32479=CARTESIAN_POINT('Ctrl Pts',(-0.145990955376697,0.0363120653110472,
0.464084209403854));
#32480=CARTESIAN_POINT('Ctrl Pts',(-0.132207444595406,0.0729769481781354,
0.462102914223418));
#32481=CARTESIAN_POINT('Ctrl Pts',(-0.107565849799547,0.0995912952759384,
0.460121619042982));
#32482=CARTESIAN_POINT('Ctrl Pts',(-0.074633794052009,0.135159819536245,
0.457473733470842));
#32483=CARTESIAN_POINT('Ctrl Pts',(-0.0223083694375825,0.15277731788608,
0.454825847898703));
#32484=CARTESIAN_POINT('Ctrl Pts',(0.0254312589463019,0.144368338990174,
0.452177962326564));
#32485=CARTESIAN_POINT('Ctrl Pts',(0.0731708873301868,0.135959360094269,
0.449530076754424));
#32486=CARTESIAN_POINT('Ctrl Pts',(0.116324719483529,0.101523903952622,
0.446882191182285));
#32487=CARTESIAN_POINT('Ctrl Pts',(0.13512098610947,0.0568421509649556,
0.444234305610146));
#32488=CARTESIAN_POINT('Ctrl Pts',(0.153917252735412,0.0121603979772891,
0.441586420038006));
#32489=CARTESIAN_POINT('Ctrl Pts',(0.148355953833953,-0.0427676518563976,
0.438938534465867));
#32490=CARTESIAN_POINT('Ctrl Pts',(0.120984436568095,-0.0827743147100686,
0.436290648893728));
#32491=CARTESIAN_POINT('Ctrl Pts',(0.0936129193022383,-0.122780977563739,
0.433642763321588));
#32492=CARTESIAN_POINT('Ctrl Pts',(0.044431183671984,-0.147866253437395,
0.430994877749449));
#32493=CARTESIAN_POINT('Ctrl Pts',(-0.0040248096733416,-0.146535421965135,
0.42834699217731));
#32494=CARTESIAN_POINT('Ctrl Pts',(-0.0524808030186669,-0.145204590492875,
0.425699106605171));
#32495=CARTESIAN_POINT('Ctrl Pts',(-0.100211054079063,-0.117457651674699,
0.423051221033031));
#32496=CARTESIAN_POINT('Ctrl Pts',(-0.125345397821707,-0.0760087182023128,
0.420403335460892));
#32497=CARTESIAN_POINT('Ctrl Pts',(-0.139070629946179,-0.0533744994995956,
0.418957391835358));
#32498=CARTESIAN_POINT('Ctrl Pts',(-0.146057814383464,-0.0266543774475973,
0.417511448209824));
#32499=CARTESIAN_POINT('Ctrl Pts',(-0.146117527463381,3.66422859593568E-5,
0.416065504584291));
#32500=CARTESIAN_POINT('Ctrl Pts',(-0.146131941026353,6.08514395597814E-5,
0.408934495415709));
#32501=CARTESIAN_POINT('Ctrl Pts',(-0.146026446689573,-0.0282099702486701,
0.410466401605588));
#32502=CARTESIAN_POINT('Ctrl Pts',(-0.138128084958642,-0.0565352970304639,
0.411998307795467));
#32503=CARTESIAN_POINT('Ctrl Pts',(-0.122817836477901,-0.0800308731172956,
0.413530213985346));
#32504=CARTESIAN_POINT('Ctrl Pts',(-0.0963247403055724,-0.120687989667408,
0.41618104869038));
#32505=CARTESIAN_POINT('Ctrl Pts',(-0.0476379432525075,-0.146883195792991,
0.418831883395415));
#32506=CARTESIAN_POINT('Ctrl Pts',(0.000888321221429993,-0.146589129065305,
0.421482718100449));
#32507=CARTESIAN_POINT('Ctrl Pts',(0.0494145856953668,-0.146295062337618,
0.424133552805483));
#32508=CARTESIAN_POINT('Ctrl Pts',(0.097780317590176,-0.119511722756663,
0.426784387510517));
#32509=CARTESIAN_POINT('Ctrl Pts',(0.123778732978107,-0.0785365161302261,
0.429435222215552));
#32510=CARTESIAN_POINT('Ctrl Pts',(0.149777148366038,-0.0375613095037888,
0.432086056920586));
#32511=CARTESIAN_POINT('Ctrl Pts',(0.15340824724709,0.0176057641681304,
0.43473689162562));
#32512=CARTESIAN_POINT('Ctrl Pts',(0.13300479146532,0.0616351303104708,
0.437387726330655));
#32513=CARTESIAN_POINT('Ctrl Pts',(0.112601335683551,0.105664496452811,
0.440038561035689));
#32514=CARTESIAN_POINT('Ctrl Pts',(0.0681633252389606,0.138556155065572,
0.442689395740723));
#32515=CARTESIAN_POINT('Ctrl Pts',(0.0200942611983476,0.145208074081285,
0.445340230445757));
#32516=CARTESIAN_POINT('Ctrl Pts',(-0.0279748028422658,0.151859993096997,
0.447991065150791));
#32517=CARTESIAN_POINT('Ctrl Pts',(-0.0796749204789013,0.132272172515661,
0.450641899855826));
#32518=CARTESIAN_POINT('Ctrl Pts',(-0.111268479500082,0.095438314693151,
0.45329273456086));
#32519=CARTESIAN_POINT('Ctrl Pts',(-0.133681961086661,0.0693071974766942,
0.455173321512477));
#32520=CARTESIAN_POINT('Ctrl Pts',(-0.145975937294016,0.0344962574238126,
0.457053908464093));
#32521=CARTESIAN_POINT('Ctrl Pts',(-0.146267142220666,-0.000128791573925899,
0.458934495415709));
#32522=CARTESIAN_POINT('Origin',(0.,0.,-0.0924367114736154));
#32523=CARTESIAN_POINT('',(-0.117750885282186,-0.00010626111879085,0.482563288526385));
#32524=CARTESIAN_POINT('',(-0.117972864089022,-5.93608753193428E-7,0.492436711473616));
#32525=CARTESIAN_POINT('',(-0.117775,-8.88924268665971E-15,-0.0924367114736154));
#32526=CARTESIAN_POINT('',(-0.117668597464311,0.00500517689817391,0.532225000000001));
#32527=CARTESIAN_POINT('Ctrl Pts',(-0.117750885282186,-0.000106261118790843,
0.482563288526385));
#32528=CARTESIAN_POINT('Ctrl Pts',(-0.117839983816431,-0.00997354393438475,
0.483229878918088));
#32529=CARTESIAN_POINT('Ctrl Pts',(-0.112189023051801,-0.0589364681957879,
0.486544354881929));
#32530=CARTESIAN_POINT('Ctrl Pts',(-0.0439766578214066,-0.132120623957634,
0.492506716417911));
#32531=CARTESIAN_POINT('Ctrl Pts',(0.087240331747497,-0.108512430051717,
0.500450373134329));
#32532=CARTESIAN_POINT('Ctrl Pts',(0.138438921804208,0.0144739368962113,
0.508394029850746));
#32533=CARTESIAN_POINT('Ctrl Pts',(0.0629040591690992,0.12431971381125,
0.516337686567165));
#32534=CARTESIAN_POINT('Ctrl Pts',(-0.0705459363093062,0.119993110375402,
0.524281343283582));
#32535=CARTESIAN_POINT('Ctrl Pts',(-0.116003159314893,0.0441585924901374,
0.529577114427861));
#32536=CARTESIAN_POINT('Ctrl Pts',(-0.117668597464311,0.00500517689817385,
0.532225));
#32537=CARTESIAN_POINT('',(-0.0334019664626897,0.112939183906319,0.532225000000001));
#32538=CARTESIAN_POINT('Origin',(0.,0.,0.532225));
#32539=CARTESIAN_POINT('Ctrl Pts',(-0.117972864533492,-5.93610086620396E-7,
0.492436711473617));
#32540=CARTESIAN_POINT('Ctrl Pts',(-0.117972892941239,-0.000127136793190444,
0.492445300790573));
#32541=CARTESIAN_POINT('Ctrl Pts',(-0.117912463615216,-0.0393074137896712,
0.495104724812564));
#32542=CARTESIAN_POINT('Ctrl Pts',(-0.0749307309976486,-0.117412744486246,
0.500414983539588));
#32543=CARTESIAN_POINT('Ctrl Pts',(0.0581614397283287,-0.126517333775439,
0.508367487654693));
#32544=CARTESIAN_POINT('Ctrl Pts',(0.138005962114904,-0.01953005209576,
0.516319991769794));
#32545=CARTESIAN_POINT('Ctrl Pts',(0.0908022345067483,0.105567300931769,
0.524272495884898));
#32546=CARTESIAN_POINT('Ctrl Pts',(0.00421962447768953,0.124065836989857,
0.529574165294966));
#32547=CARTESIAN_POINT('Ctrl Pts',(-0.0334019664626881,0.11293918390632,
0.532225));
#32548=CARTESIAN_POINT('Origin',(0.,0.,-0.0924367114736154));
#32549=CARTESIAN_POINT('',(-0.117587917984282,2.94878389348885E-5,0.432563288526385));
#32550=CARTESIAN_POINT('',(-0.117708320294082,-0.000103644876124687,0.442436711473616));
#32551=CARTESIAN_POINT('',(-0.117775,-8.88924268665971E-15,-0.0924367114736154));
#32552=CARTESIAN_POINT('Ctrl Pts',(-0.117587917984282,2.94878389348868E-5,
0.432563288526385));
#32553=CARTESIAN_POINT('Ctrl Pts',(-0.117539863949521,-0.0214500806552194,
0.434009232151918));
#32554=CARTESIAN_POINT('Ctrl Pts',(-0.101619941365326,-0.082330436444606,
0.438103061349591));
#32555=CARTESIAN_POINT('Ctrl Pts',(-0.00382300141363195,-0.139182551176009,
0.444844776119403));
#32556=CARTESIAN_POINT('Ctrl Pts',(0.11491384000461,-0.0786205074584852,
0.452788432835821));
#32557=CARTESIAN_POINT('Ctrl Pts',(0.128340187352459,0.0539893538840985,
0.460732089552239));
#32558=CARTESIAN_POINT('Ctrl Pts',(0.024156191824071,0.137125039167645,
0.468675746268657));
#32559=CARTESIAN_POINT('Ctrl Pts',(-0.0915696283436722,0.0981611996792526,
0.475952812593373));
#32560=CARTESIAN_POINT('Ctrl Pts',(-0.117486059238065,0.0292220942398885,
0.480581993345948));
#32561=CARTESIAN_POINT('Ctrl Pts',(-0.117750885282186,-0.000106261118790843,
0.482563288526385));
#32562=CARTESIAN_POINT('Ctrl Pts',(-0.117708320294082,-0.000103644876124676,
0.442436711473616));
#32563=CARTESIAN_POINT('Ctrl Pts',(-0.117804303693274,-0.0115163291952777,
0.443206959227034));
#32564=CARTESIAN_POINT('Ctrl Pts',(-0.111033657777347,-0.0620947057757177,
0.446628041685486));
#32565=CARTESIAN_POINT('Ctrl Pts',(-0.038636663810782,-0.133821400192823,
0.452699958848972));
#32566=CARTESIAN_POINT('Ctrl Pts',(0.0916608011058181,-0.104875817685159,
0.460652462964076));
#32567=CARTESIAN_POINT('Ctrl Pts',(0.137790741908166,0.0203740232160909,
0.468604967079177));
#32568=CARTESIAN_POINT('Ctrl Pts',(0.0573828398023632,0.126918127906013,
0.476557471194281));
#32569=CARTESIAN_POINT('Ctrl Pts',(-0.0755630108222985,0.116919225220885,
0.484501385992427));
#32570=CARTESIAN_POINT('Ctrl Pts',(-0.117964125743295,0.0389266160426656,
0.489794466085539));
#32571=CARTESIAN_POINT('Ctrl Pts',(-0.117972864533492,-5.93610086620396E-7,
0.492436711473617));
#32572=CARTESIAN_POINT('Origin',(0.,0.,-0.0924367114736154));
#32573=CARTESIAN_POINT('',(-0.117860863622998,9.40292562467743E-5,0.382563288526384));
#32574=CARTESIAN_POINT('',(-0.11759951728308,4.89701284099239E-5,0.392436711473616));
#32575=CARTESIAN_POINT('',(-0.117775,-8.88924268665971E-15,-0.0924367114736154));
#32576=CARTESIAN_POINT('Ctrl Pts',(-0.117860863622998,9.40292562467788E-5,
0.382563288526384));
#32577=CARTESIAN_POINT('Ctrl Pts',(-0.117574520063714,-0.0327687752160871,
0.384788585385749));
#32578=CARTESIAN_POINT('Ctrl Pts',(-0.0861467637051906,-0.105215176336211,
0.389661767817253));
#32579=CARTESIAN_POINT('Ctrl Pts',(0.0366482838797405,-0.134325140358292,
0.397182835820896));
#32580=CARTESIAN_POINT('Ctrl Pts',(0.132757756905765,-0.0419728350502109,
0.405126492537314));
#32581=CARTESIAN_POINT('Ctrl Pts',(0.107205710503746,0.0888440680441954,
0.413070149253731));
#32582=CARTESIAN_POINT('Ctrl Pts',(-0.0165914302528927,0.138242796692368,
0.42101380597015));
#32583=CARTESIAN_POINT('Ctrl Pts',(-0.105417454577164,0.0750219551131263,
0.427511519061034));
#32584=CARTESIAN_POINT('Ctrl Pts',(-0.117627862944144,0.0178843985783384,
0.431361346579779));
#32585=CARTESIAN_POINT('Ctrl Pts',(-0.117587917984282,2.94878389348868E-5,
0.432563288526385));
#32586=CARTESIAN_POINT('Ctrl Pts',(-0.11759951728308,4.89701284099274E-5,
0.392436711473616));
#32587=CARTESIAN_POINT('Ctrl Pts',(-0.11751462083269,-0.0227019422346301,
0.393968617663495));
#32588=CARTESIAN_POINT('Ctrl Pts',(-0.100159557717256,-0.0849411572528722,
0.398151358558408));
#32589=CARTESIAN_POINT('Ctrl Pts',(0.000844063931402275,-0.139284651766041,
0.404984934158356));
#32590=CARTESIAN_POINT('Ctrl Pts',(0.117610871049501,-0.0746230633995127,
0.412937438273457));
#32591=CARTESIAN_POINT('Ctrl Pts',(0.126377239427685,0.0585638604483229,
0.420889942388562));
#32592=CARTESIAN_POINT('Ctrl Pts',(0.0190929207373193,0.137972437690235,
0.428842446503664));
#32593=CARTESIAN_POINT('Ctrl Pts',(-0.0936346562739906,0.0952629110198009,
0.436024702865349));
#32594=CARTESIAN_POINT('Ctrl Pts',(-0.117473973452704,0.0277608248588199,
0.440556124522));
#32595=CARTESIAN_POINT('Ctrl Pts',(-0.117708320294082,-0.000103644876124676,
0.442436711473616));
#32596=CARTESIAN_POINT('Origin',(0.,0.,-0.0924367114736154));
#32597=CARTESIAN_POINT('',(-0.117887637745315,-8.43288998643762E-5,0.332563288526385));
#32598=CARTESIAN_POINT('',(-0.11788816540462,8.48410121138156E-5,0.342436711473616));
#32599=CARTESIAN_POINT('',(-0.117775,-8.88924268665971E-15,-0.0924367114736154));
#32600=CARTESIAN_POINT('Ctrl Pts',(-0.117887637745315,-8.43288998643547E-5,
0.332563288526385));
#32601=CARTESIAN_POINT('Ctrl Pts',(-0.117930243971446,-0.00534985313478999,
0.332920053047441));
#32602=CARTESIAN_POINT('Ctrl Pts',(-0.115216603610867,-0.0496516091215746,
0.335924703140636));
#32603=CARTESIAN_POINT('Ctrl Pts',(-0.0590623637863932,-0.126087177724698,
0.34157723880597));
#32604=CARTESIAN_POINT('Ctrl Pts',(0.0739784273282333,-0.117955633685244,
0.349520895522388));
#32605=CARTESIAN_POINT('Ctrl Pts',(0.139224117680559,-0.00172752115601949,
0.357464552238807));
#32606=CARTESIAN_POINT('Ctrl Pts',(0.0768824352591712,0.11608372080921,
0.365408208955224));
#32607=CARTESIAN_POINT('Ctrl Pts',(-0.0559156297430559,0.12751384888047,
0.373351865671643));
#32608=CARTESIAN_POINT('Ctrl Pts',(-0.114624951070718,0.0516215456314347,
0.379070225528695));
#32609=CARTESIAN_POINT('Ctrl Pts',(-0.117915240887596,0.00633474728975054,
0.382140699813609));
#32610=CARTESIAN_POINT('Ctrl Pts',(-0.117860863622998,9.40292562467788E-5,
0.382563288526384));
#32611=CARTESIAN_POINT('Ctrl Pts',(-0.11788816540462,8.4841012113826E-5,
0.342436711473616));
#32612=CARTESIAN_POINT('Ctrl Pts',(-0.1176132193427,-0.0337657100314819,
0.344730276099956));
#32613=CARTESIAN_POINT('Ctrl Pts',(-0.0845149237619996,-0.107208837865588,
0.34967467543133));
#32614=CARTESIAN_POINT('Ctrl Pts',(0.0402561631274929,-0.133343040355529,
0.357269909467738));
#32615=CARTESIAN_POINT('Ctrl Pts',(0.133929618074243,-0.0382594079720193,
0.365222413582842));
#32616=CARTESIAN_POINT('Ctrl Pts',(0.104617274119081,0.0919573329132998,
0.373174917697944));
#32617=CARTESIAN_POINT('Ctrl Pts',(-0.020763734615072,0.137730870367254,
0.381127421813047));
#32618=CARTESIAN_POINT('Ctrl Pts',(-0.106598215372521,0.0725739208566139,
0.387548019738271));
#32619=CARTESIAN_POINT('Ctrl Pts',(-0.117661526993468,0.0166665964275914,
0.391317782958461));
#32620=CARTESIAN_POINT('Ctrl Pts',(-0.11759951728308,4.89701284099274E-5,
0.392436711473616));
#32621=CARTESIAN_POINT('Origin',(0.,0.,-0.0924367114736154));
#32622=CARTESIAN_POINT('',(-0.117597135791184,-4.46042773137295E-5,0.282563288526384));
#32623=CARTESIAN_POINT('',(-0.117869129870917,-9.20611903598989E-5,0.292436711473616));
#32624=CARTESIAN_POINT('',(-0.117775,-8.88924268665971E-15,-0.0924367114736154));
#32625=CARTESIAN_POINT('Ctrl Pts',(-0.117597135791184,-4.46042773137294E-5,
0.282563288526384));
#32626=CARTESIAN_POINT('Ctrl Pts',(-0.117654518243026,-0.0169184081852861,
0.283699406281271));
#32627=CARTESIAN_POINT('Ctrl Pts',(-0.106362773508523,-0.0730457989372372,
0.287483409608297));
#32628=CARTESIAN_POINT('Ctrl Pts',(-0.0200165152988323,-0.137788527592198,
0.293915298507463));
#32629=CARTESIAN_POINT('Ctrl Pts',(0.104968269293632,-0.0914767820950745,
0.301858955223881));
#32630=CARTESIAN_POINT('Ctrl Pts',(0.133758329466478,0.0386658573002006,
0.309802611940298));
#32631=CARTESIAN_POINT('Ctrl Pts',(0.0399699596916912,0.133374441107753,
0.317746268656717));
#32632=CARTESIAN_POINT('Ctrl Pts',(-0.084590271720082,0.107092283864913,
0.325333160852078));
#32633=CARTESIAN_POINT('Ctrl Pts',(-0.117614023033548,0.0337305621770822,
0.330272167475301));
#32634=CARTESIAN_POINT('Ctrl Pts',(-0.117887637745315,-8.43288998643547E-5,
0.332563288526385));
#32635=CARTESIAN_POINT('Ctrl Pts',(-0.117869129870917,-9.2061190359885E-5,
0.292436711473616));
#32636=CARTESIAN_POINT('Ctrl Pts',(-0.117920440224669,-0.00606290911736031,
0.292841099831383));
#32637=CARTESIAN_POINT('Ctrl Pts',(-0.114789890532149,-0.0511197142210238,
0.295896322894184));
#32638=CARTESIAN_POINT('Ctrl Pts',(-0.0566691588697243,-0.127238089669758,
0.301602380662019));
#32639=CARTESIAN_POINT('Ctrl Pts',(0.0763719541489209,-0.116482829853556,
0.309554884777122));
#32640=CARTESIAN_POINT('Ctrl Pts',(0.139281709756163,0.00123707506708643,
0.317507388892225));
#32641=CARTESIAN_POINT('Ctrl Pts',(0.0742909098282569,0.117820990265484,
0.325459893007327));
#32642=CARTESIAN_POINT('Ctrl Pts',(-0.0589202520252667,0.1262114453589,
0.33341239712243));
#32643=CARTESIAN_POINT('Ctrl Pts',(-0.115211084829427,0.0497097039247984,
0.339071336611193));
#32644=CARTESIAN_POINT('Ctrl Pts',(-0.11793099393452,0.00535776373524371,
0.342079441394922));
#32645=CARTESIAN_POINT('Ctrl Pts',(-0.11788816540462,8.4841012113826E-5,
0.342436711473616));
#32646=CARTESIAN_POINT('Origin',(0.,0.,-0.0924367114736154));
#32647=CARTESIAN_POINT('',(-0.117724026649356,0.00010549178999148,0.232563288526384));
#32648=CARTESIAN_POINT('',(-0.117591763024586,-3.83449468523145E-5,0.242436711473616));
#32649=CARTESIAN_POINT('',(-0.117775,-8.88924268665971E-15,-0.0924367114736154));
#32650=CARTESIAN_POINT('Ctrl Pts',(-0.117724026649356,0.000105491789991495,
0.232563288526384));
#32651=CARTESIAN_POINT('Ctrl Pts',(-0.117478226080151,-0.0282662610808501,
0.234478759515102));
#32652=CARTESIAN_POINT('Ctrl Pts',(-0.0929369215417509,-0.0962395631396471,
0.239042116075959));
#32653=CARTESIAN_POINT('Ctrl Pts',(0.0207448421498254,-0.137680756627218,
0.246253358208955));
#32654=CARTESIAN_POINT('Ctrl Pts',(0.126961839902422,-0.0571579428392388,
0.254197014925373));
#32655=CARTESIAN_POINT('Ctrl Pts',(0.116828827462796,0.075745391244066,
0.262140671641791));
#32656=CARTESIAN_POINT('Ctrl Pts',(-0.000368128572008151,0.139234348141551,
0.270084328358209));
#32657=CARTESIAN_POINT('Ctrl Pts',(-0.100514230788311,0.0842953826634335,
0.27689186731974));
#32658=CARTESIAN_POINT('Ctrl Pts',(-0.117520780198996,0.0224084148687892,
0.281051520709132));
#32659=CARTESIAN_POINT('Ctrl Pts',(-0.117597135791184,-4.46042773137294E-5,
0.282563288526384));
#32660=CARTESIAN_POINT('Ctrl Pts',(-0.117591763024586,-3.83449468523075E-5,
0.242436711473616));
#32661=CARTESIAN_POINT('Ctrl Pts',(-0.117642174491994,-0.017358594045656,
0.243602758267844));
#32662=CARTESIAN_POINT('Ctrl Pts',(-0.10593062496396,-0.0739889980249599,
0.247419639767106));
#32663=CARTESIAN_POINT('Ctrl Pts',(-0.0183140487741412,-0.138077951344142,
0.253887355971402));
#32664=CARTESIAN_POINT('Ctrl Pts',(0.106234136865658,-0.0900845891054932,
0.261839860086505));
#32665=CARTESIAN_POINT('Ctrl Pts',(0.133228916899009,0.040632262203075,
0.269792364201608));
#32666=CARTESIAN_POINT('Ctrl Pts',(0.0378813411502606,0.134037043471229,
0.27774486831671));
#32667=CARTESIAN_POINT('Ctrl Pts',(-0.085634823441202,0.105866601183683,
0.285292984074047));
#32668=CARTESIAN_POINT('Ctrl Pts',(-0.117584092098319,0.0330770181317487,
0.290190265126349));
#32669=CARTESIAN_POINT('Ctrl Pts',(-0.117869129870917,-9.2061190359885E-5,
0.292436711473616));
#32670=CARTESIAN_POINT('Origin',(0.,0.,-0.0924367114736154));
#32671=CARTESIAN_POINT('',(-0.117966882359366,-1.29211934964908E-5,0.182563288526384));
#32672=CARTESIAN_POINT('',(-0.117728105208174,0.000106637828744482,0.192436711473616));
#32673=CARTESIAN_POINT('',(-0.117775,-8.88924268665971E-15,-0.0924367114736154));
#32674=CARTESIAN_POINT('Ctrl Pts',(-0.117966882359366,-1.29211934964912E-5,
0.182563288526384));
#32675=CARTESIAN_POINT('Ctrl Pts',(-0.117967957119725,-0.000704465266726215,
0.182610227176794));
#32676=CARTESIAN_POINT('Ctrl Pts',(-0.117649070375187,-0.0404061166150831,
0.185305051399342));
#32677=CARTESIAN_POINT('Ctrl Pts',(-0.0733536600413758,-0.118345172107485,
0.19064776119403));
#32678=CARTESIAN_POINT('Ctrl Pts',(0.0597282696676458,-0.12577310138558,
0.198591417910448));
#32679=CARTESIAN_POINT('Ctrl Pts',(0.138074187460599,-0.0179404007303906,
0.206535074626866));
#32680=CARTESIAN_POINT('Ctrl Pts',(0.0898865489335327,0.106333191146418,
0.214478731343283));
#32681=CARTESIAN_POINT('Ctrl Pts',(-0.0406746665030564,0.133161220808791,
0.222422388059702));
#32682=CARTESIAN_POINT('Ctrl Pts',(-0.111466604862902,0.0609145729578186,
0.228450573787402));
#32683=CARTESIAN_POINT('Ctrl Pts',(-0.117818012892196,0.0109539388206346,
0.231830873942963));
#32684=CARTESIAN_POINT('Ctrl Pts',(-0.117724026649356,0.000105491789991495,
0.232563288526384));
#32685=CARTESIAN_POINT('Ctrl Pts',(-0.117728105208174,0.000106637828744488,
0.192436711473616));
#32686=CARTESIAN_POINT('Ctrl Pts',(-0.11747787316262,-0.0284437724366353,
0.194364416704305));
#32687=CARTESIAN_POINT('Ctrl Pts',(-0.0926723165398222,-0.0966441001570621,
0.198942956640028));
#32688=CARTESIAN_POINT('Ctrl Pts',(0.0215406810767683,-0.137611496939632,
0.206172331280785));
#32689=CARTESIAN_POINT('Ctrl Pts',(0.127397488829925,-0.056309900280862,
0.214124835395888));
#32690=CARTESIAN_POINT('Ctrl Pts',(0.116266864218555,0.0767003345124148,
0.222077339510991));
#32691=CARTESIAN_POINT('Ctrl Pts',(-0.0016300870944122,0.139277664563073,
0.230029843626094));
#32692=CARTESIAN_POINT('Ctrl Pts',(-0.100962832358778,0.0835357163242542,
0.236816300946969));
#32693=CARTESIAN_POINT('Ctrl Pts',(-0.117527571486354,0.0220164272984534,
0.240951923562809));
#32694=CARTESIAN_POINT('Ctrl Pts',(-0.117591763024586,-3.83449468523075E-5,
0.242436711473616));
#32695=CARTESIAN_POINT('Origin',(0.,0.,-0.0924367114736154));
#32696=CARTESIAN_POINT('',(-0.117685857408994,-9.79219620674319E-5,0.132563288526384));
#32697=CARTESIAN_POINT('',(-0.117968412270431,-1.06668654225733E-5,0.142436711473616));
#32698=CARTESIAN_POINT('',(-0.117775,-8.88924268665971E-15,-0.0924367114736154));
#32699=CARTESIAN_POINT('Ctrl Pts',(-0.117685857408994,-9.79219620674231E-5,
0.132563288526384));
#32700=CARTESIAN_POINT('Ctrl Pts',(-0.117781952389543,-0.0123469217649596,
0.133389580410625));
#32701=CARTESIAN_POINT('Ctrl Pts',(-0.110383000729775,-0.063735125339128,
0.136863757867004));
#32702=CARTESIAN_POINT('Ctrl Pts',(-0.03593748288359,-0.134517045800752,
0.142985820895522));
#32703=CARTESIAN_POINT('Ctrl Pts',(0.0935927050428541,-0.103086105216301,
0.150929477611941));
#32704=CARTESIAN_POINT('Ctrl Pts',(0.137352931996012,0.0228147184504364,
0.158873134328358));
#32705=CARTESIAN_POINT('Ctrl Pts',(0.0552405729858772,0.127807739141585,
0.166816791044776));
#32706=CARTESIAN_POINT('Ctrl Pts',(-0.0767108666901454,0.115747243191764,
0.174713509110785));
#32707=CARTESIAN_POINT('Ctrl Pts',(-0.117907328140755,0.0383066600647174,
0.179962341604654));
#32708=CARTESIAN_POINT('Ctrl Pts',(-0.117966882359366,-1.29211934964912E-5,
0.182563288526384));
#32709=CARTESIAN_POINT('Ctrl Pts',(-0.117968412270431,-1.06668654225827E-5,
0.142436711473616));
#32710=CARTESIAN_POINT('Ctrl Pts',(-0.117969144731522,-0.000578292161741028,
0.142475240435732));
#32711=CARTESIAN_POINT('Ctrl Pts',(-0.117707998838203,-0.0401984655398319,
0.145164604102881));
#32712=CARTESIAN_POINT('Ctrl Pts',(-0.0736248085349355,-0.118238371369349,
0.150504802475065));
#32713=CARTESIAN_POINT('Ctrl Pts',(0.0596315829014974,-0.125876921640408,
0.158457306590168));
#32714=CARTESIAN_POINT('Ctrl Pts',(0.138129079193178,-0.0179243554725553,
0.166409810705271));
#32715=CARTESIAN_POINT('Ctrl Pts',(0.0897844651888838,0.106487909275724,
0.174362314820374));
#32716=CARTESIAN_POINT('Ctrl Pts',(-0.0410080379701501,0.133113732800722,
0.182314818935477));
#32717=CARTESIAN_POINT('Ctrl Pts',(-0.111567175621,0.0606792399755161,0.188339617819891));
#32718=CARTESIAN_POINT('Ctrl Pts',(-0.117821973380904,0.0108165964048154,
0.19171358199927));
#32719=CARTESIAN_POINT('Ctrl Pts',(-0.117728105208174,0.000106637828744488,
0.192436711473616));
#32720=CARTESIAN_POINT('Origin',(0.,0.,-0.0924367114736154));
#32721=CARTESIAN_POINT('',(-0.117616583813332,6.45879523355414E-5,0.0825632885263843));
#32722=CARTESIAN_POINT('',(-0.117696063073914,-0.000101172369946279,0.092436711473616));
#32723=CARTESIAN_POINT('',(-0.117775,-8.88924268665971E-15,-0.0924367114736154));
#32724=CARTESIAN_POINT('Ctrl Pts',(-0.117616583813332,6.4587952335533E-5,
0.0825632885263843));
#32725=CARTESIAN_POINT('Ctrl Pts',(-0.117498290532644,-0.023772899795338,
0.0841689336444552));
#32726=CARTESIAN_POINT('Ctrl Pts',(-0.0988756392612849,-0.087091103874762,
0.0884224643346654));
#32727=CARTESIAN_POINT('Ctrl Pts',(0.00455872999049264,-0.139160029798142,
0.0953238805970148));
#32728=CARTESIAN_POINT('Ctrl Pts',(0.119435794773867,-0.0715642270726515,
0.103267537313433));
#32729=CARTESIAN_POINT('Ctrl Pts',(0.124859895376695,0.0616145512171006,
0.111211194029851));
#32730=CARTESIAN_POINT('Ctrl Pts',(0.0158602180480347,0.138328544685192,
0.119154850746269));
#32731=CARTESIAN_POINT('Ctrl Pts',(-0.094824103560013,0.0934823880103396,
0.126272215578446));
#32732=CARTESIAN_POINT('Ctrl Pts',(-0.117474012159943,0.0269054906934358,
0.130741694838485));
#32733=CARTESIAN_POINT('Ctrl Pts',(-0.117685857408994,-9.79219620674231E-5,
0.132563288526384));
#32734=CARTESIAN_POINT('Ctrl Pts',(-0.117696063073914,-0.000101172369946261,
0.092436711473616));
#32735=CARTESIAN_POINT('Ctrl Pts',(-0.117792623998916,-0.0119605829319943,
0.0932368988721926));
#32736=CARTESIAN_POINT('Ctrl Pts',(-0.110686607712821,-0.0629944099979452,
0.0966879209758034));
#32737=CARTESIAN_POINT('Ctrl Pts',(-0.0371242974264225,-0.134248668971966,
0.102789777784449));
#32738=CARTESIAN_POINT('Ctrl Pts',(0.0928396337021713,-0.10383510521762,
0.110742281899551));
#32739=CARTESIAN_POINT('Ctrl Pts',(0.137550169005636,0.0219289054269618,
0.118694786014654));
#32740=CARTESIAN_POINT('Ctrl Pts',(0.0559501922162531,0.127555870431356,
0.126647290129757));
#32741=CARTESIAN_POINT('Ctrl Pts',(-0.0763838391282559,0.116105719252975,
0.134561265282744));
#32742=CARTESIAN_POINT('Ctrl Pts',(-0.117918750607874,0.0384749486295239,
0.139824405730697));
#32743=CARTESIAN_POINT('Ctrl Pts',(-0.117968412270431,-1.06668654225827E-5,
0.142436711473616));
#32744=CARTESIAN_POINT('Origin',(0.,0.,-0.0924367114736154));
#32745=CARTESIAN_POINT('',(-0.117919967015755,7.48285734863531E-5,0.0325632885263843));
#32746=CARTESIAN_POINT('',(-0.117605093279175,5.63740904734461E-5,0.042436711473616));
#32747=CARTESIAN_POINT('',(-0.117775,-8.88924268665971E-15,-0.0924367114736154));
#32748=CARTESIAN_POINT('Ctrl Pts',(-0.117919967015755,7.48285734863559E-5,
0.0325632885263843));
#32749=CARTESIAN_POINT('Ctrl Pts',(-0.117681732256532,-0.0350969523534404,
0.0349482868782861));
#32750=CARTESIAN_POINT('Ctrl Pts',(-0.0823020584651488,-0.1097611636214,
0.0399811708023271));
#32751=CARTESIAN_POINT('Ctrl Pts',(0.0446654385229893,-0.131869273048715,
0.0476619402985074));
#32752=CARTESIAN_POINT('Ctrl Pts',(0.135042047193827,-0.033912683303242,
0.0556055970149253));
#32753=CARTESIAN_POINT('Ctrl Pts',(0.101666114468308,0.0951356880412728,
0.0635492537313433));
#32754=CARTESIAN_POINT('Ctrl Pts',(-0.0248796065525388,0.136992916606216,
0.0714929104477611));
#32755=CARTESIAN_POINT('Ctrl Pts',(-0.107654697213721,0.0702257630245385,
0.0778309220461081));
#32756=CARTESIAN_POINT('Ctrl Pts',(-0.117693369175918,0.0155377418730691,
0.0815210480723159));
#32757=CARTESIAN_POINT('Ctrl Pts',(-0.117616583813332,6.4587952335533E-5,
0.0825632885263843));
#32758=CARTESIAN_POINT('Ctrl Pts',(-0.117605093279175,5.6374090473453E-5,
0.042436711473616));
#32759=CARTESIAN_POINT('Ctrl Pts',(-0.117506950346121,-0.0231366833782073,
0.0439985573086537));
#32760=CARTESIAN_POINT('Ctrl Pts',(-0.0996401976376468,-0.0858346907547986,
0.0482112378487256));
#32761=CARTESIAN_POINT('Ctrl Pts',(0.00241643506700816,-0.139265216174241,
0.0550747530938317));
#32762=CARTESIAN_POINT('Ctrl Pts',(0.118445458723555,-0.0732914200146354,
0.0630272572089346));
#32763=CARTESIAN_POINT('Ctrl Pts',(0.125708256673902,0.0599868231457294,
0.0709797613240373));
#32764=CARTESIAN_POINT('Ctrl Pts',(0.0175344664057042,0.138178956948752,
0.0789322654391402));
#32765=CARTESIAN_POINT('Ctrl Pts',(-0.0942361274410431,0.0943834610594897,
0.0860845821556665));
#32766=CARTESIAN_POINT('Ctrl Pts',(-0.117472740117216,0.0273268854223547,
0.0905860641671583));
#32767=CARTESIAN_POINT('Ctrl Pts',(-0.117696063073914,-0.000101172369946261,
0.092436711473616));
#32768=CARTESIAN_POINT('Origin',(0.,0.,0.55));
#32769=CARTESIAN_POINT('',(-0.143213254968838,-6.38556725402083E-7,0.507000235761732));
#32770=CARTESIAN_POINT('Ctrl Pts',(-0.0334019664626817,0.112939183906321,
0.532225));
#32771=CARTESIAN_POINT('Ctrl Pts',(-0.025060850432499,0.115799622360937,
0.531847620192936));
#32772=CARTESIAN_POINT('Ctrl Pts',(-0.0164290366846974,0.117635249741265,
0.531473612813392));
#32773=CARTESIAN_POINT('Ctrl Pts',(-0.00767275263448023,0.118510014194121,
0.531100586051555));
#32774=CARTESIAN_POINT('Ctrl Pts',(-0.00421690952474848,0.118855257529045,
0.530953363558858));
#32775=CARTESIAN_POINT('Ctrl Pts',(-0.000739669302851069,0.119050301419728,
0.530806218229583));
#32776=CARTESIAN_POINT('Ctrl Pts',(0.00274357664202706,0.119096927952431,
0.530659241408731));
#32777=CARTESIAN_POINT('Ctrl Pts',(0.00973382066470735,0.119190498962541,
0.5303642855372));
#32778=CARTESIAN_POINT('Ctrl Pts',(0.0167166427004772,0.118687723090435,
0.530071327820757));
#32779=CARTESIAN_POINT('Ctrl Pts',(0.023612882680227,0.11761343656186,0.529779224661465));
#32780=CARTESIAN_POINT('Ctrl Pts',(0.0274136336191392,0.117021360946144,
0.529618236737583));
#32781=CARTESIAN_POINT('Ctrl Pts',(0.0311881579134606,0.116255363574116,
0.529457508384123));
#32782=CARTESIAN_POINT('Ctrl Pts',(0.0349231679080101,0.115317271371855,
0.529296848155877));
#32783=CARTESIAN_POINT('Ctrl Pts',(0.037971953630239,0.114551532560831,
0.529165705639333));
#32784=CARTESIAN_POINT('Ctrl Pts',(0.0409939934565533,0.113670841591964,
0.529034622190513));
#32785=CARTESIAN_POINT('Ctrl Pts',(0.0439689729533011,0.112680856226694,
0.528904071147902));
#32786=CARTESIAN_POINT('Ctrl Pts',(0.0505577881110133,0.110488293021555,
0.528614934133899));
#32787=CARTESIAN_POINT('Ctrl Pts',(0.0569328249215936,0.107756906396238,
0.528327689901185));
#32788=CARTESIAN_POINT('Ctrl Pts',(0.0630179104963209,0.104502120084129,
0.528041256645784));
#32789=CARTESIAN_POINT('Ctrl Pts',(0.0668676595642169,0.102442968997859,
0.527860043720435));
#32790=CARTESIAN_POINT('Ctrl Pts',(0.0706013360983203,0.100173990889927,
0.527679155388847));
#32791=CARTESIAN_POINT('Ctrl Pts',(0.0741982818595768,0.0976957705995567,
0.527498317717128));
#32792=CARTESIAN_POINT('Ctrl Pts',(0.0762868294587642,0.0962568050489885,
0.527393315276118));
#32793=CARTESIAN_POINT('Ctrl Pts',(0.0783301222953497,0.0947465519651971,
0.527288283929736));
#32794=CARTESIAN_POINT('Ctrl Pts',(0.0803210903525092,0.0931669243552789,
0.527183314414725));
#32795=CARTESIAN_POINT('Ctrl Pts',(0.0873333522084643,0.0876034185040368,
0.526813607967904));
#32796=CARTESIAN_POINT('Ctrl Pts',(0.0936466399845286,0.0812254488323135,
0.526447434844115));
#32797=CARTESIAN_POINT('Ctrl Pts',(0.0992257444432458,0.0742158265894858,
0.526082561055055));
#32798=CARTESIAN_POINT('Ctrl Pts',(0.101943770530818,0.0708008813664647,
0.525904801974781));
#32799=CARTESIAN_POINT('Ctrl Pts',(0.104487132714136,0.0672353052679948,
0.525727351283807));
#32800=CARTESIAN_POINT('Ctrl Pts',(0.106849003984973,0.0635370592318222,
0.525549950667934));
#32801=CARTESIAN_POINT('Ctrl Pts',(0.108451822333258,0.0610273472604538,
0.525429562666425));
#32802=CARTESIAN_POINT('Ctrl Pts',(0.109972218146102,0.0584542637442968,
0.525309095710787));
#32803=CARTESIAN_POINT('Ctrl Pts',(0.111403508282751,0.0558304813946845,
0.525188806889777));
#32804=CARTESIAN_POINT('Ctrl Pts',(0.115946659550801,0.0475021629053002,
0.524806990306466));
#32805=CARTESIAN_POINT('Ctrl Pts',(0.119574294719482,0.0387078320373927,
0.524428851599571));
#32806=CARTESIAN_POINT('Ctrl Pts',(0.122229265704535,0.02963297991244,0.524051927142185));
#32807=CARTESIAN_POINT('Ctrl Pts',(0.123491040005696,0.0253201586942182,
0.523872793887439));
#32808=CARTESIAN_POINT('Ctrl Pts',(0.124532521003962,0.0209434889498052,
0.523693934885913));
#32809=CARTESIAN_POINT('Ctrl Pts',(0.125343829183128,0.0165211886089503,
0.523515085689393));
#32810=CARTESIAN_POINT('Ctrl Pts',(0.126073723283802,0.0125426623065107,
0.523354183856031));
#32811=CARTESIAN_POINT('Ctrl Pts',(0.126617185118597,0.00852274589339418,
0.523193115530006));
#32812=CARTESIAN_POINT('Ctrl Pts',(0.126964066890117,0.00450317609134152,
0.523032822082874));
#32813=CARTESIAN_POINT('Ctrl Pts',(0.127610380106321,-0.00298612228009172,
0.522734161899901));
#32814=CARTESIAN_POINT('Ctrl Pts',(0.127580071374667,-0.0104910608890547,
0.522437493943663));
#32815=CARTESIAN_POINT('Ctrl Pts',(0.126833825603371,-0.0179253657039838,
0.52214162882945));
#32816=CARTESIAN_POINT('Ctrl Pts',(0.126370997360361,-0.0225361874571381,
0.521958130662699));
#32817=CARTESIAN_POINT('Ctrl Pts',(0.125632379838884,-0.0271199619342287,
0.521774941316387));
#32818=CARTESIAN_POINT('Ctrl Pts',(0.124632255285918,-0.0316602427367966,
0.52159177704026));
#32819=CARTESIAN_POINT('Ctrl Pts',(0.123677051866189,-0.0359965943804856,
0.521416839686298));
#32820=CARTESIAN_POINT('Ctrl Pts',(0.122480780227546,-0.0402989646849493,
0.521241685776095));
#32821=CARTESIAN_POINT('Ctrl Pts',(0.121065837229724,-0.044520244829744,
0.521067408183846));
#32822=CARTESIAN_POINT('Ctrl Pts',(0.118338362465597,-0.0526572758514579,
0.520731466922931));
#32823=CARTESIAN_POINT('Ctrl Pts',(0.114798640009948,-0.0605127756442529,
0.520398022841861));
#32824=CARTESIAN_POINT('Ctrl Pts',(0.11054080941355,-0.0679858568570343,
0.520065383890604));
#32825=CARTESIAN_POINT('Ctrl Pts',(0.108372779925159,-0.0717910482735648,
0.5198960086562));
#32826=CARTESIAN_POINT('Ctrl Pts',(0.10601800718922,-0.0754969965361626,
0.51972684216845));
#32827=CARTESIAN_POINT('Ctrl Pts',(0.103485875290119,-0.0790891197455118,
0.519557661047695));
#32828=CARTESIAN_POINT('Ctrl Pts',(0.101239265068231,-0.0822761972920135,
0.519407556688845));
#32829=CARTESIAN_POINT('Ctrl Pts',(0.0988505693656959,-0.0853758696950735,
0.519257316754896));
#32830=CARTESIAN_POINT('Ctrl Pts',(0.0963426843438634,-0.0883583266502687,
0.51910776182463));
#32831=CARTESIAN_POINT('Ctrl Pts',(0.0906830843157466,-0.0950889037383469,
0.518770257880003));
#32832=CARTESIAN_POINT('Ctrl Pts',(0.084404823468622,-0.101245530098652,
0.518435260730044));
#32833=CARTESIAN_POINT('Ctrl Pts',(0.077590384105458,-0.106717161154373,
0.51810105566737));
#32834=CARTESIAN_POINT('Ctrl Pts',(0.072812396824573,-0.110553629893275,
0.517866725672845));
#32835=CARTESIAN_POINT('Ctrl Pts',(0.0677701261881638,-0.114053116790221,
0.517632785084427));
#32836=CARTESIAN_POINT('Ctrl Pts',(0.0624852082906241,-0.117169678449436,
0.517398642838002));
#32837=CARTESIAN_POINT('Ctrl Pts',(0.060232694538615,-0.11849800523378,
0.517298847790998));
#32838=CARTESIAN_POINT('Ctrl Pts',(0.0579421351333471,-0.119753052219492,
0.517199285984453));
#32839=CARTESIAN_POINT('Ctrl Pts',(0.0556164103289471,-0.120931647626768,
0.517099943244175));
#32840=CARTESIAN_POINT('Ctrl Pts',(0.0470766353824801,-0.125259304756293,
0.516735168941155));
#32841=CARTESIAN_POINT('Ctrl Pts',(0.0380619111816488,-0.128561628767388,
0.516373216300106));
#32842=CARTESIAN_POINT('Ctrl Pts',(0.0287540615399164,-0.13087769180711,
0.516011917283344));
#32843=CARTESIAN_POINT('Ctrl Pts',(0.0244834739512418,-0.131940337901829,
0.515846147620515));
#32844=CARTESIAN_POINT('Ctrl Pts',(0.0201508023558736,-0.132794720803219,
0.515680515553343));
#32845=CARTESIAN_POINT('Ctrl Pts',(0.0157724288157125,-0.133441328903782,
0.515514811679433));
#32846=CARTESIAN_POINT('Ctrl Pts',(0.0127414878228209,-0.13388894512025,
0.515400102721983));
#32847=CARTESIAN_POINT('Ctrl Pts',(0.0096905970655013,-0.134236406792975,
0.515285434752076));
#32848=CARTESIAN_POINT('Ctrl Pts',(0.00663678161128016,-0.134483505205774,
0.515171166690044));
#32849=CARTESIAN_POINT('Ctrl Pts',(-0.00335208404858516,-0.135291750788136,
0.514797402021565));
#32850=CARTESIAN_POINT('Ctrl Pts',(-0.0134050142894213,-0.135035519709951,
0.514426646108251));
#32851=CARTESIAN_POINT('Ctrl Pts',(-0.0233297246571887,-0.13373576937046,
0.514056571073779));
#32852=CARTESIAN_POINT('Ctrl Pts',(-0.0275876193693317,-0.133178151073044,
0.5138978016514));
#32853=CARTESIAN_POINT('Ctrl Pts',(-0.0318220223293205,-0.132427814053447,
0.513739157550061));
#32854=CARTESIAN_POINT('Ctrl Pts',(-0.0360175989408762,-0.131483472271743,
0.513580454950452));
#32855=CARTESIAN_POINT('Ctrl Pts',(-0.0391091145169674,-0.130787632915777,
0.513463514752696));
#32856=CARTESIAN_POINT('Ctrl Pts',(-0.0421792587373029,-0.12998615137042,
0.513346550232001));
#32857=CARTESIAN_POINT('Ctrl Pts',(-0.0452082926810733,-0.129082949079949,
0.513230012664731));
#32858=CARTESIAN_POINT('Ctrl Pts',(-0.0547989520179786,-0.126223190608758,
0.512861026338271));
#32859=CARTESIAN_POINT('Ctrl Pts',(-0.0640135938008781,-0.122340292920341,
0.512494993993967));
#32860=CARTESIAN_POINT('Ctrl Pts',(-0.0726621826878073,-0.117434240919462,
0.512129678956248));
#32861=CARTESIAN_POINT('Ctrl Pts',(-0.0732258670681981,-0.11711448183293,
0.512105869016456));
#32862=CARTESIAN_POINT('Ctrl Pts',(-0.073787141143001,-0.116790358750658,
0.512082062123761));
#32863=CARTESIAN_POINT('Ctrl Pts',(-0.0743459493499517,-0.11646186427858,
0.5120582576589));
#32864=CARTESIAN_POINT('Ctrl Pts',(-0.0780940452153038,-0.11425855237787,
0.511898593904482));
#32865=CARTESIAN_POINT('Ctrl Pts',(-0.0817313018976771,-0.111858709629848,
0.511739039373249));
#32866=CARTESIAN_POINT('Ctrl Pts',(-0.085250803842968,-0.109275770384611,
0.511579407204066));
#32867=CARTESIAN_POINT('Ctrl Pts',(-0.0875213278289363,-0.107609447819153,
0.511476424260826));
#32868=CARTESIAN_POINT('Ctrl Pts',(-0.0897413530091093,-0.105867722400153,
0.511373470200391));
#32869=CARTESIAN_POINT('Ctrl Pts',(-0.0919020268850941,-0.104060687103246,
0.511270839257698));
#32870=CARTESIAN_POINT('Ctrl Pts',(-0.0994865656445924,-0.0977175136139456,
0.510910577410027));
#32871=CARTESIAN_POINT('Ctrl Pts',(-0.106368098520952,-0.0905540945926997,
0.510553119515254));
#32872=CARTESIAN_POINT('Ctrl Pts',(-0.112476669881714,-0.082740585635558,
0.510196385012091));
#32873=CARTESIAN_POINT('Ctrl Pts',(-0.115701946031867,-0.0786151162581588,
0.510008032086826));
#32874=CARTESIAN_POINT('Ctrl Pts',(-0.118711292938496,-0.0743076837297934,
0.509819880825374));
#32875=CARTESIAN_POINT('Ctrl Pts',(-0.121490605137305,-0.0698396458594739,
0.509631624987483));
#32876=CARTESIAN_POINT('Ctrl Pts',(-0.123158603264919,-0.0671581627195108,
0.509518643658775));
#32877=CARTESIAN_POINT('Ctrl Pts',(-0.124742701375389,-0.0644198867277164,
0.509405676189658));
#32878=CARTESIAN_POINT('Ctrl Pts',(-0.126234357059848,-0.06164059243669,
0.509293097144302));
#32879=CARTESIAN_POINT('Ctrl Pts',(-0.131306921574689,-0.0521892493795411,
0.508910257809098));
#32880=CARTESIAN_POINT('Ctrl Pts',(-0.135335100093566,-0.0422336175385342,
0.508530533331389));
#32881=CARTESIAN_POINT('Ctrl Pts',(-0.138212265982587,-0.0319628814891436,
0.508151426353207));
#32882=CARTESIAN_POINT('Ctrl Pts',(-0.139343321582236,-0.0279253063303673,
0.508002393907016));
#32883=CARTESIAN_POINT('Ctrl Pts',(-0.140295939750969,-0.0238387054236251,
0.507853456888584));
#32884=CARTESIAN_POINT('Ctrl Pts',(-0.14106118303298,-0.0197137190414539,
0.507704463579619));
#32885=CARTESIAN_POINT('Ctrl Pts',(-0.141663078970186,-0.0164692442413196,
0.507587274093027));
#32886=CARTESIAN_POINT('Ctrl Pts',(-0.142148737315268,-0.0132004963364534,
0.507470032942495));
#32887=CARTESIAN_POINT('Ctrl Pts',(-0.14251240365623,-0.00992818124989041,
0.507353216880015));
#32888=CARTESIAN_POINT('Ctrl Pts',(-0.14286252481498,-0.00677774740200931,
0.507240751769694));
#32889=CARTESIAN_POINT('Ctrl Pts',(-0.143100295244155,-0.00362062020727709,
0.507128557913111));
#32890=CARTESIAN_POINT('Ctrl Pts',(-0.143222931917338,-0.0004616047295162,
0.507016572073626));
#32891=CARTESIAN_POINT('Ctrl Pts',(-0.143228895796354,-0.000307980323141247,
0.507011126149655));
#32892=CARTESIAN_POINT('Ctrl Pts',(-0.143234587305958,-0.000154351422170947,
0.50700568071763));
#32893=CARTESIAN_POINT('Ctrl Pts',(-0.143240006909252,-7.18572550341278E-7,
0.507000235770275));
#32894=CARTESIAN_POINT('',(-0.00156805256656782,0.146109107730171,0.50365));
#32895=CARTESIAN_POINT('Ctrl Pts',(-0.0015703316452181,0.146071601053478,
0.50365));
#32896=CARTESIAN_POINT('Ctrl Pts',(-0.0117120407853717,0.144648246558049,
0.504950624278524));
#32897=CARTESIAN_POINT('Ctrl Pts',(-0.0216505365241647,0.142222557694311,
0.506260995613922));
#32898=CARTESIAN_POINT('Ctrl Pts',(-0.0312063389538959,0.13880538472021,
0.507590209176103));
#32899=CARTESIAN_POINT('Ctrl Pts',(-0.0379631701734481,0.136389129130603,
0.508530085419929));
#32900=CARTESIAN_POINT('Ctrl Pts',(-0.0445284394867549,0.133476109724793,
0.50947938238263));
#32901=CARTESIAN_POINT('Ctrl Pts',(-0.050827361354341,0.13005807034167,
0.510441315490383));
#32902=CARTESIAN_POINT('Ctrl Pts',(-0.0535603409840707,0.12857504956382,
0.510858679547901));
#32903=CARTESIAN_POINT('Ctrl Pts',(-0.056235007151428,0.127001156165417,
0.511277203939051));
#32904=CARTESIAN_POINT('Ctrl Pts',(-0.0588447172056459,0.125337452214503,
0.511696981696819));
#32905=CARTESIAN_POINT('Ctrl Pts',(-0.0624191770014244,0.123058715204999,
0.512271941629964));
#32906=CARTESIAN_POINT('Ctrl Pts',(-0.0658727208815536,0.120611069028702,
0.512849385708712));
#32907=CARTESIAN_POINT('Ctrl Pts',(-0.0691906694557284,0.117994047416377,
0.513430106410014));
#32908=CARTESIAN_POINT('Ctrl Pts',(-0.0733832729377804,0.114687144467415,
0.51416391273038));
#32909=CARTESIAN_POINT('Ctrl Pts',(-0.0773595119772722,0.111109779201256,
0.514902950893669));
#32910=CARTESIAN_POINT('Ctrl Pts',(-0.0811052238678245,0.107288843574283,
0.515648819828442));
#32911=CARTESIAN_POINT('Ctrl Pts',(-0.0841017207582698,0.104232169153142,
0.516245500515327));
#32912=CARTESIAN_POINT('Ctrl Pts',(-0.0869506135922833,0.101019546539762,
0.516846552684068));
#32913=CARTESIAN_POINT('Ctrl Pts',(-0.0896425492995218,0.097664267789728,
0.517452794926569));
#32914=CARTESIAN_POINT('Ctrl Pts',(-0.0913307146861822,0.0955601070428074,
0.517832981261246));
#32915=CARTESIAN_POINT('Ctrl Pts',(-0.0929559105919431,0.0934010507133458,
0.518214974249558));
#32916=CARTESIAN_POINT('Ctrl Pts',(-0.094511034598742,0.0911980939617143,
0.518597709131816));
#32917=CARTESIAN_POINT('Ctrl Pts',(-0.0989061554610084,0.0849720559509604,
0.519679401690337));
#32918=CARTESIAN_POINT('Ctrl Pts',(-0.102756278369653,0.0783797189661076,
0.520769927597638));
#32919=CARTESIAN_POINT('Ctrl Pts',(-0.106019480011838,0.0715022869017531,
0.521874709646989));
#32920=CARTESIAN_POINT('Ctrl Pts',(-0.10810684462629,0.0671030159085511,
0.522581403014228));
#32921=CARTESIAN_POINT('Ctrl Pts',(-0.109953633570546,0.0625869322502571,
0.523293929634644));
#32922=CARTESIAN_POINT('Ctrl Pts',(-0.111544021459737,0.0579753350677128,
0.524013708847662));
#32923=CARTESIAN_POINT('Ctrl Pts',(-0.11291963712523,0.0539865060717378,
0.524636286250227));
#32924=CARTESIAN_POINT('Ctrl Pts',(-0.114104149138597,0.0499208096400247,
0.525265113718246));
#32925=CARTESIAN_POINT('Ctrl Pts',(-0.115079157041328,0.0458232444145113,
0.525896440126774));
#32926=CARTESIAN_POINT('Ctrl Pts',(-0.117097797518837,0.0373397121269415,
0.527203528037759));
#32927=CARTESIAN_POINT('Ctrl Pts',(-0.118231089846825,0.0286982113614575,
0.528524583654289));
#32928=CARTESIAN_POINT('Ctrl Pts',(-0.118391363114938,0.0200276346563605,
0.529869408057975));
#32929=CARTESIAN_POINT('Ctrl Pts',(-0.118483921504357,0.0150203453896601,
0.530646048993314));
#32930=CARTESIAN_POINT('Ctrl Pts',(-0.118251089036742,0.0100034984621487,
0.531430617066573));
#32931=CARTESIAN_POINT('Ctrl Pts',(-0.117668597464311,0.00500517689817885,
0.532225));
#32932=CARTESIAN_POINT('',(-0.115076068242798,0.0902060425677366,0.50365));
#32933=CARTESIAN_POINT('Origin',(0.,0.,0.50365));
#32934=CARTESIAN_POINT('Ctrl Pts',(-0.143240006909252,-7.18572550341278E-7,
0.507000235770275));
#32935=CARTESIAN_POINT('Ctrl Pts',(-0.143520908694302,0.00796217822295569,
0.506718020385041));
#32936=CARTESIAN_POINT('Ctrl Pts',(-0.14307308860376,0.0159355469497794,
0.506437106818574));
#32937=CARTESIAN_POINT('Ctrl Pts',(-0.141950240996583,0.0238446282639654,
0.506156482679269));
#32938=CARTESIAN_POINT('Ctrl Pts',(-0.141327877173321,0.0282284164590215,
0.506000940367809));
#32939=CARTESIAN_POINT('Ctrl Pts',(-0.140497759623186,0.0325924948231262,
0.505845486973662));
#32940=CARTESIAN_POINT('Ctrl Pts',(-0.139466483050223,0.0369239027928834,
0.505689950104037));
#32941=CARTESIAN_POINT('Ctrl Pts',(-0.138800760016326,0.0397199694642927,
0.50558954592591));
#32942=CARTESIAN_POINT('Ctrl Pts',(-0.138051361267828,0.0425008441913541,
0.50548916176982));
#32943=CARTESIAN_POINT('Ctrl Pts',(-0.137223245651255,0.0452539885083259,
0.505389082377033));
#32944=CARTESIAN_POINT('Ctrl Pts',(-0.134183880382411,0.0553586297560613,
0.505021769136614));
#32945=CARTESIAN_POINT('Ctrl Pts',(-0.130080477516678,0.06512485891418,
0.504657328869907));
#32946=CARTESIAN_POINT('Ctrl Pts',(-0.125019236367424,0.0743847486871139,
0.504293559587933));
#32947=CARTESIAN_POINT('Ctrl Pts',(-0.122033398952289,0.0798475441810871,
0.504078956904408));
#32948=CARTESIAN_POINT('Ctrl Pts',(-0.118713161823888,0.0851340339476938,
0.503864587744543));
#32949=CARTESIAN_POINT('Ctrl Pts',(-0.115072616245007,0.0902061753896176,
0.50365));
#32950=CARTESIAN_POINT('',(-0.05,-6.12323399573676E-18,0.6));
#32951=CARTESIAN_POINT('',(-0.1,-1.22464679914735E-17,0.55));
#32952=CARTESIAN_POINT('Origin',(0.,0.,0.6));
#32953=CARTESIAN_POINT('Ctrl Pts',(0.0850780204044556,-0.119080027477571,
-0.0164977839420937));
#32954=CARTESIAN_POINT('Ctrl Pts',(0.124701079614845,-0.0907709019978731,
-0.0138498983699544));
#32955=CARTESIAN_POINT('Ctrl Pts',(0.172780327456066,0.00801716155080004,
-0.00855412722567576));
#32956=CARTESIAN_POINT('Ctrl Pts',(0.0867037234097596,0.149857524855506,
-0.000610470509257829));
#32957=CARTESIAN_POINT('Ctrl Pts',(-0.0789008477636886,0.153920736728128,
0.00733318620716008));
#32958=CARTESIAN_POINT('Ctrl Pts',(-0.172161895422237,0.0171520622219753,
0.015276842923578));
#32959=CARTESIAN_POINT('Ctrl Pts',(-0.107670523249975,-0.135451540092597,
0.0232204996399959));
#32960=CARTESIAN_POINT('Ctrl Pts',(0.0555023301026467,-0.163863876974566,
0.0311641563564139));
#32961=CARTESIAN_POINT('Ctrl Pts',(0.167806441153186,-0.042140702198512,
0.0391078130728317));
#32962=CARTESIAN_POINT('Ctrl Pts',(0.126332717914983,0.118217855613161,
0.0470514697892497));
#32963=CARTESIAN_POINT('Ctrl Pts',(-0.0309159874248675,0.170230637616809,
0.0549951265056676));
#32964=CARTESIAN_POINT('Ctrl Pts',(-0.159831956410111,0.066245824895792,
0.0629387832220855));
#32965=CARTESIAN_POINT('Ctrl Pts',(-0.14227559413168,-0.0984502643440673,
0.0708824399385034));
#32966=CARTESIAN_POINT('Ctrl Pts',(0.00566478568548768,-0.172923543714354,
0.0788260966549214));
#32967=CARTESIAN_POINT('Ctrl Pts',(0.148413742858461,-0.0889274008243077,
0.0867697533713393));
#32968=CARTESIAN_POINT('Ctrl Pts',(0.155153858530075,0.0765636983283585,
0.0947134100877573));
#32969=CARTESIAN_POINT('Ctrl Pts',(0.0197082819896427,0.171890320651054,
0.102657066804175));
#32970=CARTESIAN_POINT('Ctrl Pts',(-0.133798285716779,0.109693800981729,
0.110600723520593));
#32971=CARTESIAN_POINT('Ctrl Pts',(-0.164689815771182,-0.0530280538225922,
0.118544380237011));
#32972=CARTESIAN_POINT('Ctrl Pts',(-0.044656766037051,-0.167154062007556,
0.126488036953429));
#32973=CARTESIAN_POINT('Ctrl Pts',(0.11630050845274,-0.128097231996654,
0.134431693669847));
#32974=CARTESIAN_POINT('Ctrl Pts',(0.170678001253376,0.0283501086412318,
0.142375350386265));
#32975=CARTESIAN_POINT('Ctrl Pts',(0.0686432422541576,0.158816918899349,
0.150319007102683));
#32976=CARTESIAN_POINT('Ctrl Pts',(-0.0962973622855325,0.143741179688805,
0.1582626638191));
#32977=CARTESIAN_POINT('Ctrl Pts',(-0.172989410659926,-0.00306144592864502,
0.166206320535519));
#32978=CARTESIAN_POINT('Ctrl Pts',(-0.0911509925455794,-0.147058509343496,
0.174149977251936));
#32979=CARTESIAN_POINT('Ctrl Pts',(0.0742197602705133,-0.1562886299111,
0.182093633968354));
#32980=CARTESIAN_POINT('Ctrl Pts',(0.171574250349044,-0.0222931661803689,
0.190037290684772));
#32981=CARTESIAN_POINT('Ctrl Pts',(0.111695151232628,0.132132137756553,
0.19798094740119));
#32982=CARTESIAN_POINT('Ctrl Pts',(-0.0505433024217535,0.165469281811646,
0.205924604117608));
#32983=CARTESIAN_POINT('Ctrl Pts',(-0.16646300584434,0.0471675346608595,
0.213868260834026));
#32984=CARTESIAN_POINT('Ctrl Pts',(-0.129833152315396,-0.11435935117077,
0.221811917550444));
#32985=CARTESIAN_POINT('Ctrl Pts',(0.0257780314041745,-0.171085363892111,
0.229755574266861));
#32986=CARTESIAN_POINT('Ctrl Pts',(0.157765784501968,-0.0710258113735757,
0.23769923098328));
#32987=CARTESIAN_POINT('Ctrl Pts',(0.145174263631334,0.0941230142947892,
0.245642887699697));
#32988=CARTESIAN_POINT('Ctrl Pts',(-0.000457445268631668,0.173015893445265,
0.253586544416116));
#32989=CARTESIAN_POINT('Ctrl Pts',(-0.145669943468849,0.0933540369270586,
0.261530201132533));
#32990=CARTESIAN_POINT('Ctrl Pts',(-0.15738800412666,-0.0718590620464598,
0.269473857848952));
#32991=CARTESIAN_POINT('Ctrl Pts',(-0.0248729952365478,-0.171219282641631,
0.277417514565369));
#32992=CARTESIAN_POINT('Ctrl Pts',(0.130436053586269,-0.11367121256306,
0.285361171281788));
#32993=CARTESIAN_POINT('Ctrl Pts',(0.166211263149388,0.0480471086044073,
0.293304827998205));
#32994=CARTESIAN_POINT('Ctrl Pts',(0.0496676170739063,0.16573423439711,
0.301248484714623));
#32995=CARTESIAN_POINT('Ctrl Pts',(-0.112392286114514,0.131539661939415,
0.309192141431041));
#32996=CARTESIAN_POINT('Ctrl Pts',(-0.171453968444308,-0.0232001154910803,
0.317135798147459));
#32997=CARTESIAN_POINT('Ctrl Pts',(-0.0733922898759408,-0.156678908596981,
0.325079454863877));
#32998=CARTESIAN_POINT('Ctrl Pts',(0.0919273431499614,-0.146574459688691,
0.333023111580294));
#32999=CARTESIAN_POINT('Ctrl Pts',(0.173003180832518,-0.00214665863879225,
0.340966768296713));
#33000=CARTESIAN_POINT('Ctrl Pts',(0.0955359320753977,0.14424837648421,
0.34891042501313));
#33001=CARTESIAN_POINT('Ctrl Pts',(-0.0694820837435447,0.158451723911329,
0.356854081729549));
#33002=CARTESIAN_POINT('Ctrl Pts',(-0.170825527907542,0.0274471879557805,
0.364797738445966));
#33003=CARTESIAN_POINT('Ctrl Pts',(-0.115621519313607,-0.128710417100276,
0.372741395162384));
#33004=CARTESIAN_POINT('Ctrl Pts',(0.0455400241630207,-0.16691559576681,
0.380685051878803));
#33005=CARTESIAN_POINT('Ctrl Pts',(0.164967928025121,-0.0521564373559641,
0.38862870859522));
#33006=CARTESIAN_POINT('Ctrl Pts',(0.133216350942249,0.110399739828213,
0.396572365311638));
#33007=CARTESIAN_POINT('Ctrl Pts',(-0.0206169035662114,0.171783768167507,
0.404516022028056));
#33008=CARTESIAN_POINT('Ctrl Pts',(-0.155556614414135,0.0757420715232724,
0.412459678744474));
#33009=CARTESIAN_POINT('Ctrl Pts',(-0.14794130513946,-0.0897107128565239,
0.420403335460892));
#33010=CARTESIAN_POINT('Ctrl Pts',(-0.00475055195827078,-0.17295152931105,
0.42834699217731));
#33011=CARTESIAN_POINT('Ctrl Pts',(0.142794654932494,-0.0976957016900834,
0.436290648893728));
#33012=CARTESIAN_POINT('Ctrl Pts',(0.159478551636871,0.0670884478109748,
0.444234305610146));
#33013=CARTESIAN_POINT('Ctrl Pts',(0.0300170551768464,0.170394816235914,
0.452177962326563));
#33014=CARTESIAN_POINT('Ctrl Pts',(-0.126959218666436,0.117542321186412,
0.460121619042982));
#33015=CARTESIAN_POINT('Ctrl Pts',(-0.167575279308382,-0.043016329325927,
0.468065275759399));
#33016=CARTESIAN_POINT('Ctrl Pts',(-0.054646434915416,-0.164176211557628,
0.476008932475817));
#33017=CARTESIAN_POINT('Ctrl Pts',(0.108406899182729,-0.134840111552273,
0.483952589192236));
#33018=CARTESIAN_POINT('Ctrl Pts',(0.172027477869207,0.0179856562492908,
0.491896245908652));
#33019=CARTESIAN_POINT('Ctrl Pts',(0.0781660714022324,0.154482616143293,
0.499839902625072));
#33020=CARTESIAN_POINT('Ctrl Pts',(-0.0876620486424683,0.149106276403653,
0.507783559341488));
#33021=CARTESIAN_POINT('Ctrl Pts',(-0.144148268866352,0.0548725112369506,
0.513079330485768));
#33022=CARTESIAN_POINT('Ctrl Pts',(-0.146217781693075,0.00621955117001058,
0.515727216057907));
#33023=CARTESIAN_POINT('Ctrl Pts',(0.0795408277542857,-0.111329858282327,
-0.0109985226280625));
#33024=CARTESIAN_POINT('Ctrl Pts',(0.116585071529219,-0.0848631955302966,
-0.00835063705592319));
#33025=CARTESIAN_POINT('Ctrl Pts',(0.161535143861813,0.00749537498591264,
-0.00305486591164458));
#33026=CARTESIAN_POINT('Ctrl Pts',(0.0810607239872927,0.140104242147965,
0.00488879080477336));
#33027=CARTESIAN_POINT('Ctrl Pts',(-0.0737656883858339,0.143903005144011,
0.0128324475211912));
#33028=CARTESIAN_POINT('Ctrl Pts',(-0.160956961675077,0.0160357424907528,
0.0207761042376092));
#33029=CARTESIAN_POINT('Ctrl Pts',(-0.100662926844399,-0.12663585222528,
0.028719760954027));
#33030=CARTESIAN_POINT('Ctrl Pts',(0.0518900329094276,-0.153199008999282,
0.0366634176704451));
#33031=CARTESIAN_POINT('Ctrl Pts',(0.156884976500066,-0.039398029233422,
0.0446070743868629));
#33032=CARTESIAN_POINT('Ctrl Pts',(0.118110516766091,0.110523799755865,
0.052550731103281));
#33033=CARTESIAN_POINT('Ctrl Pts',(-0.0289038604674246,0.159151397279945,
0.0604943878196987));
#33034=CARTESIAN_POINT('Ctrl Pts',(-0.149429500757181,0.0619343012734311,
0.0684380445361168));
#33035=CARTESIAN_POINT('Ctrl Pts',(-0.133015771554951,-0.0920427565348621,
0.0763817012525346));
#33036=CARTESIAN_POINT('Ctrl Pts',(0.00529610045382266,-0.161669039075616,
0.0843253579689526));
#33037=CARTESIAN_POINT('Ctrl Pts',(0.138754426830263,-0.0831396762404221,
0.0922690146853704));
#33038=CARTESIAN_POINT('Ctrl Pts',(0.145055870812282,0.0715806492912723,
0.100212671401788));
#33039=CARTESIAN_POINT('Ctrl Pts',(0.0184255940091067,0.160703061995767,
0.108156328118206));
#33040=CARTESIAN_POINT('Ctrl Pts',(-0.125090197766985,0.102554522168261,
0.116099984834624));
#33041=CARTESIAN_POINT('Ctrl Pts',(-0.153971192640191,-0.0495767916930391,
0.124043641551042));
#33042=CARTESIAN_POINT('Ctrl Pts',(-0.0417503383192307,-0.156275056605288,
0.13198729826746));
#33043=CARTESIAN_POINT('Ctrl Pts',(0.108731240649445,-0.119760189736536,
0.139930954983878));
#33044=CARTESIAN_POINT('Ctrl Pts',(0.159569644834255,0.0265049785776333,
0.147874611700296));
#33045=CARTESIAN_POINT('Ctrl Pts',(0.0641756858313974,0.148480525646761,
0.155818268416713));
#33046=CARTESIAN_POINT('Ctrl Pts',(-0.0900299733154633,0.134385971376294,
0.163761925133132));
#33047=CARTESIAN_POINT('Ctrl Pts',(-0.161730619156435,-0.00286219568969563,
0.171705581849549));
#33048=CARTESIAN_POINT('Ctrl Pts',(-0.0852185483775114,-0.137487396931492,
0.179649238565968));
#33049=CARTESIAN_POINT('Ctrl Pts',(0.0693892634028907,-0.14611678706926,
0.187592895282385));
#33050=CARTESIAN_POINT('Ctrl Pts',(0.160407562719562,-0.0208422443637096,
0.195536551998804));
#33051=CARTESIAN_POINT('Ctrl Pts',(0.104425617132929,0.123532488886508,
0.203480208715221));
#33052=CARTESIAN_POINT('Ctrl Pts',(-0.0472537571155211,0.154699928144028,
0.211423865431639));
#33053=CARTESIAN_POINT('Ctrl Pts',(-0.155628976936467,0.0440976968224941,
0.219367522148057));
#33054=CARTESIAN_POINT('Ctrl Pts',(-0.121383129932039,-0.106916421072365,
0.227311178864475));
#33055=CARTESIAN_POINT('Ctrl Pts',(0.0241003016527248,-0.159950494803813,
0.235254835580893));
#33056=CARTESIAN_POINT('Ctrl Pts',(0.147497802968786,-0.0664031885287967,
0.243198492297311));
#33057=CARTESIAN_POINT('Ctrl Pts',(0.135725784908488,0.0879971399445481,
0.251142149013729));
#33058=CARTESIAN_POINT('Ctrl Pts',(-0.000427673036423806,0.161755378344027,
0.259085805730147));
#33059=CARTESIAN_POINT('Ctrl Pts',(-0.136189204066452,0.0872782104717779,
0.267029462446565));
#33060=CARTESIAN_POINT('Ctrl Pts',(-0.147144609939394,-0.067182208161988,
0.274973119162982));
#33061=CARTESIAN_POINT('Ctrl Pts',(-0.0232541685906426,-0.160075697625154,
0.282916775879401));
#33062=CARTESIAN_POINT('Ctrl Pts',(0.12194679215539,-0.106273069073731,
0.290860432595819));
#33063=CARTESIAN_POINT('Ctrl Pts',(0.155393618588418,0.0449200248363383,
0.298804089312236));
#33064=CARTESIAN_POINT('Ctrl Pts',(0.0464350646131678,0.154947636633991,
0.306747746028654));
#33065=CARTESIAN_POINT('Ctrl Pts',(-0.105077379894898,0.122978573589753,
0.314691402745072));
#33066=CARTESIAN_POINT('Ctrl Pts',(-0.160295109206645,-0.021690166054439,
0.32263505946149));
#33067=CARTESIAN_POINT('Ctrl Pts',(-0.0686156478460915,-0.146481664972887,
0.330578716177908));
#33068=CARTESIAN_POINT('Ctrl Pts',(0.0859443712093853,-0.137034851020875,
0.338522372894326));
#33069=CARTESIAN_POINT('Ctrl Pts',(0.161743493115198,-0.00200694614453471,
0.346466029610744));
#33070=CARTESIAN_POINT('Ctrl Pts',(0.0893180998033222,0.134860157925877,
0.354409686327162));
#33071=CARTESIAN_POINT('Ctrl Pts',(-0.0649599324100484,0.148139098901043,
0.36235334304358));
#33072=CARTESIAN_POINT('Ctrl Pts',(-0.159707569907411,0.0256608233143121,
0.370296999759998));
#33073=CARTESIAN_POINT('Ctrl Pts',(-0.108096442638088,-0.120333466482715,
0.378240656476415));
#33074=CARTESIAN_POINT('Ctrl Pts',(0.0425761107352605,-0.156052110630637,
0.386184313192834));
#33075=CARTESIAN_POINT('Ctrl Pts',(0.154231204318669,-0.0487619032540464,
0.394127969909251));
#33076=CARTESIAN_POINT('Ctrl Pts',(0.124546137462748,0.103214515900207,
0.402071626625669));
#33077=CARTESIAN_POINT('Ctrl Pts',(-0.0192750791284384,0.160603444342461,
0.410015283342087));
#33078=CARTESIAN_POINT('Ctrl Pts',(-0.145432413851821,0.0708124970015145,
0.417958940058505));
#33079=CARTESIAN_POINT('Ctrl Pts',(-0.138312737107664,-0.0838720074246256,
0.425902596774923));
#33080=CARTESIAN_POINT('Ctrl Pts',(-0.00444136844339109,-0.161695203266036,
0.433846253491342));
#33081=CARTESIAN_POINT('Ctrl Pts',(0.133501049956532,-0.0913373036128839,
0.441789910207758));
#33082=CARTESIAN_POINT('Ctrl Pts',(0.1490990968754,0.0627220831686826,0.449733566924177));
#33083=CARTESIAN_POINT('Ctrl Pts',(0.0280634340592545,0.159304890546491,
0.457677223640594));
#33084=CARTESIAN_POINT('Ctrl Pts',(-0.118696242528426,0.109892231611416,
0.465620880357014));
#33085=CARTESIAN_POINT('Ctrl Pts',(-0.156668859524218,-0.0402166673045443,
0.47356453707343));
#33086=CARTESIAN_POINT('Ctrl Pts',(-0.0510898425507461,-0.153491015690964,
0.481508193789849));
#33087=CARTESIAN_POINT('Ctrl Pts',(0.101351376704318,-0.126064217718754,
0.489451850506266));
#33088=CARTESIAN_POINT('Ctrl Pts',(0.160831292514208,0.0168150831315976,
0.497395507222684));
#33089=CARTESIAN_POINT('Ctrl Pts',(0.0730787339911879,0.144428315365945,
0.505339163939102));
#33090=CARTESIAN_POINT('Ctrl Pts',(-0.0819566778647476,0.13940188772757,
0.51328282065552));
#33091=CARTESIAN_POINT('Ctrl Pts',(-0.134766565682532,0.0513012049880128,
0.518578591799799));
#33092=CARTESIAN_POINT('Ctrl Pts',(-0.136701386950153,0.005814759746065,
0.521226477371938));
#33093=CARTESIAN_POINT('Ctrl Pts',(0.0740036351041157,-0.103579689087084,
-0.00549926131403131));
#33094=CARTESIAN_POINT('Ctrl Pts',(0.108469063443593,-0.0789554890627202,
-0.00285137574189201));
#33095=CARTESIAN_POINT('Ctrl Pts',(0.150289960267559,0.00697358842102527,
0.00244439540238661));
#33096=CARTESIAN_POINT('Ctrl Pts',(0.0754177245648256,0.130350959440424,
0.0103880521188046));
#33097=CARTESIAN_POINT('Ctrl Pts',(-0.0686305290079791,0.133885273559895,
0.0183317088352224));
#33098=CARTESIAN_POINT('Ctrl Pts',(-0.149752027927918,0.0149194227595303,
0.0262753655516404));
#33099=CARTESIAN_POINT('Ctrl Pts',(-0.0936553304388222,-0.117820164357962,
0.0342190222680582));
#33100=CARTESIAN_POINT('Ctrl Pts',(0.0482777357162085,-0.142534141023999,
0.0421626789844763));
#33101=CARTESIAN_POINT('Ctrl Pts',(0.145963511846947,-0.036655356268332,
0.050106335700894));
#33102=CARTESIAN_POINT('Ctrl Pts',(0.1098883156172,0.102829743898569,0.0580499924173122));
#33103=CARTESIAN_POINT('Ctrl Pts',(-0.0268917335099817,0.14807215694308,
0.0659936491337298));
#33104=CARTESIAN_POINT('Ctrl Pts',(-0.139027045104252,0.0576227776510703,
0.073937305850148));
#33105=CARTESIAN_POINT('Ctrl Pts',(-0.123755948978222,-0.0856352487256572,
0.0818809625665656));
#33106=CARTESIAN_POINT('Ctrl Pts',(0.00492741522215772,-0.150414534436879,
0.0898246192829839));
#33107=CARTESIAN_POINT('Ctrl Pts',(0.129095110802064,-0.0773519516565369,
0.0977682759994015));
#33108=CARTESIAN_POINT('Ctrl Pts',(0.134957883094489,0.0665976002541865,
0.10571193271582));
#33109=CARTESIAN_POINT('Ctrl Pts',(0.0171429060285707,0.14951580334048,
0.113655589432237));
#33110=CARTESIAN_POINT('Ctrl Pts',(-0.116382109817192,0.0954152433547932,
0.121599246148655));
#33111=CARTESIAN_POINT('Ctrl Pts',(-0.1432525695092,-0.046125529563486,
0.129542902865073));
#33112=CARTESIAN_POINT('Ctrl Pts',(-0.0388439106014103,-0.14539605120302,
0.137486559581491));
#33113=CARTESIAN_POINT('Ctrl Pts',(0.101161972846149,-0.111423147476419,
0.145430216297909));
#33114=CARTESIAN_POINT('Ctrl Pts',(0.148461288415133,0.0246598485140348,
0.153373873014327));
#33115=CARTESIAN_POINT('Ctrl Pts',(0.0597081294086373,0.138144132394173,
0.161317529730745));
#33116=CARTESIAN_POINT('Ctrl Pts',(-0.0837625843453943,0.125030763063784,
0.169261186447163));
#33117=CARTESIAN_POINT('Ctrl Pts',(-0.150471827652945,-0.00266294545074625,
0.177204843163581));
#33118=CARTESIAN_POINT('Ctrl Pts',(-0.0792861042094436,-0.127916284519489,
0.185148499879999));
#33119=CARTESIAN_POINT('Ctrl Pts',(0.0645587665352683,-0.13594494422742,
0.193092156596417));
#33120=CARTESIAN_POINT('Ctrl Pts',(0.149240875090081,-0.01939132254705,
0.201035813312835));
#33121=CARTESIAN_POINT('Ctrl Pts',(0.0971560830332309,0.114932840016463,
0.208979470029252));
#33122=CARTESIAN_POINT('Ctrl Pts',(-0.0439642118092888,0.143930574476409,
0.216923126745671));
#33123=CARTESIAN_POINT('Ctrl Pts',(-0.144794948028593,0.0410278589841287,
0.224866783462088));
#33124=CARTESIAN_POINT('Ctrl Pts',(-0.112933107548683,-0.0994734909739605,
0.232810440178506));
#33125=CARTESIAN_POINT('Ctrl Pts',(0.0224225719012751,-0.148815625715515,
0.240754096894924));
#33126=CARTESIAN_POINT('Ctrl Pts',(0.137229821435604,-0.0617805656840178,
0.248697753611342));
#33127=CARTESIAN_POINT('Ctrl Pts',(0.126277306185642,0.081871265594307,
0.25664141032776));
#33128=CARTESIAN_POINT('Ctrl Pts',(-0.000397900804215911,0.150494863242789,
0.264585067044178));
#33129=CARTESIAN_POINT('Ctrl Pts',(-0.126708464664056,0.0812023840164973,
0.272528723760596));
#33130=CARTESIAN_POINT('Ctrl Pts',(-0.136901215752127,-0.0625053542775162,
0.280472380477014));
#33131=CARTESIAN_POINT('Ctrl Pts',(-0.0216353419447375,-0.148932112608676,
0.288416037193432));
#33132=CARTESIAN_POINT('Ctrl Pts',(0.113457530724511,-0.0988749255844029,
0.29635969390985));
#33133=CARTESIAN_POINT('Ctrl Pts',(0.144575974027448,0.0417929410682694,
0.304303350626268));
#33134=CARTESIAN_POINT('Ctrl Pts',(0.0432025121524296,0.144161038870872,
0.312247007342686));
#33135=CARTESIAN_POINT('Ctrl Pts',(-0.0977624736752833,0.114417485240091,
0.320190664059103));
#33136=CARTESIAN_POINT('Ctrl Pts',(-0.149136249968981,-0.0201802166177978,
0.328134320775522));
#33137=CARTESIAN_POINT('Ctrl Pts',(-0.0638390058162424,-0.136284421348793,
0.336077977491939));
#33138=CARTESIAN_POINT('Ctrl Pts',(0.0799613992688094,-0.127495242353059,
0.344021634208357));
#33139=CARTESIAN_POINT('Ctrl Pts',(0.150483805397878,-0.00186723365027712,
0.351965290924775));
#33140=CARTESIAN_POINT('Ctrl Pts',(0.0831002675312467,0.125471939367544,
0.359908947641193));
#33141=CARTESIAN_POINT('Ctrl Pts',(-0.0604377810765522,0.137826473890756,
0.367852604357611));
#33142=CARTESIAN_POINT('Ctrl Pts',(-0.148589611907278,0.0238744586728436,
0.375796261074029));
#33143=CARTESIAN_POINT('Ctrl Pts',(-0.100571365962569,-0.111956515865154,
0.383739917790446));
#33144=CARTESIAN_POINT('Ctrl Pts',(0.0396121973075005,-0.145188625494464,
0.391683574506865));
#33145=CARTESIAN_POINT('Ctrl Pts',(0.143494480612217,-0.0453673691521286,
0.399627231223282));
#33146=CARTESIAN_POINT('Ctrl Pts',(0.115875923983247,0.0960292919722012,
0.407570887939701));
#33147=CARTESIAN_POINT('Ctrl Pts',(-0.0179332546906655,0.149423120517415,
0.415514544656118));
#33148=CARTESIAN_POINT('Ctrl Pts',(-0.135308213289508,0.0658829224797566,
0.423458201372536));
#33149=CARTESIAN_POINT('Ctrl Pts',(-0.128684169075867,-0.0780333019927274,
0.431401858088955));
#33150=CARTESIAN_POINT('Ctrl Pts',(-0.0041321849285115,-0.150438877221023,
0.439345514805372));
#33151=CARTESIAN_POINT('Ctrl Pts',(0.124207444980571,-0.0849789055356846,
0.44728917152179));
#33152=CARTESIAN_POINT('Ctrl Pts',(0.13871964211393,0.0583557185263908,
0.455232828238208));
#33153=CARTESIAN_POINT('Ctrl Pts',(0.0261098129416626,0.148214964857068,
0.463176484954626));
#33154=CARTESIAN_POINT('Ctrl Pts',(-0.110433266390416,0.10224214203642,
0.471120141671043));
#33155=CARTESIAN_POINT('Ctrl Pts',(-0.145762439740054,-0.0374170052831618,
0.479063798387463));
#33156=CARTESIAN_POINT('Ctrl Pts',(-0.0475332501860763,-0.142805819824299,
0.487007455103879));
#33157=CARTESIAN_POINT('Ctrl Pts',(0.0942958542259076,-0.117288323885235,
0.494951111820298));
#33158=CARTESIAN_POINT('Ctrl Pts',(0.149635107159208,0.0156445100139045,
0.502894768536715));
#33159=CARTESIAN_POINT('Ctrl Pts',(0.0679913965801436,0.134374014588598,
0.510838425253134));
#33160=CARTESIAN_POINT('Ctrl Pts',(-0.0762513070870269,0.129697499051486,
0.518782081969551));
#33161=CARTESIAN_POINT('Ctrl Pts',(-0.125384862498713,0.0477298987390752,
0.52407785311383));
#33162=CARTESIAN_POINT('Ctrl Pts',(-0.127184992207232,0.00540996832211942,
0.526725738685969));
#33163=CARTESIAN_POINT('Ctrl Pts',(0.0684664424539458,-0.0958295198918399,
-1.2490009027033E-16));
#33164=CARTESIAN_POINT('Ctrl Pts',(0.100353055357967,-0.0730477825951437,
0.00264788557213918));
#33165=CARTESIAN_POINT('Ctrl Pts',(0.139044776673305,0.00645180185613777,
0.00794365671641779));
#33166=CARTESIAN_POINT('Ctrl Pts',(0.0697747251423586,0.120597676732883,
0.0158873134328358));
#33167=CARTESIAN_POINT('Ctrl Pts',(-0.0634953696301243,0.123867541975778,
0.0238309701492536));
#33168=CARTESIAN_POINT('Ctrl Pts',(-0.138547094180758,0.0138031030283078,
0.0317746268656716));
#33169=CARTESIAN_POINT('Ctrl Pts',(-0.0866477340332458,-0.109004476490645,
0.0397182835820895));
#33170=CARTESIAN_POINT('Ctrl Pts',(0.0446654385229893,-0.131869273048715,
0.0476619402985074));
#33171=CARTESIAN_POINT('Ctrl Pts',(0.135042047193827,-0.033912683303242,
0.0556055970149253));
#33172=CARTESIAN_POINT('Ctrl Pts',(0.101666114468308,0.0951356880412728,
0.0635492537313433));
#33173=CARTESIAN_POINT('Ctrl Pts',(-0.0248796065525388,0.136992916606216,
0.0714929104477611));
#33174=CARTESIAN_POINT('Ctrl Pts',(-0.128624589451322,0.0533112540287094,
0.079436567164179));
#33175=CARTESIAN_POINT('Ctrl Pts',(-0.114496126401493,-0.079227740916452,
0.087380223880597));
#33176=CARTESIAN_POINT('Ctrl Pts',(0.00455872999049264,-0.139160029798142,
0.0953238805970148));
#33177=CARTESIAN_POINT('Ctrl Pts',(0.119435794773867,-0.0715642270726515,
0.103267537313433));
#33178=CARTESIAN_POINT('Ctrl Pts',(0.124859895376695,0.0616145512171006,
0.111211194029851));
#33179=CARTESIAN_POINT('Ctrl Pts',(0.0158602180480347,0.138328544685192,
0.119154850746269));
#33180=CARTESIAN_POINT('Ctrl Pts',(-0.107674021867399,0.0882759645413252,
0.127098507462686));
#33181=CARTESIAN_POINT('Ctrl Pts',(-0.132533946378209,-0.0426742674339329,
0.135042164179105));
#33182=CARTESIAN_POINT('Ctrl Pts',(-0.03593748288359,-0.134517045800752,
0.142985820895522));
#33183=CARTESIAN_POINT('Ctrl Pts',(0.0935927050428541,-0.103086105216301,
0.150929477611941));
#33184=CARTESIAN_POINT('Ctrl Pts',(0.137352931996012,0.0228147184504364,
0.158873134328358));
#33185=CARTESIAN_POINT('Ctrl Pts',(0.0552405729858772,0.127807739141585,
0.166816791044776));
#33186=CARTESIAN_POINT('Ctrl Pts',(-0.0774951953753252,0.115675554751273,
0.174760447761194));
#33187=CARTESIAN_POINT('Ctrl Pts',(-0.139213036149455,-0.00246369521179678,
0.182704104477612));
#33188=CARTESIAN_POINT('Ctrl Pts',(-0.0733536600413758,-0.118345172107485,
0.19064776119403));
#33189=CARTESIAN_POINT('Ctrl Pts',(0.0597282696676458,-0.12577310138558,
0.198591417910448));
#33190=CARTESIAN_POINT('Ctrl Pts',(0.138074187460599,-0.0179404007303906,
0.206535074626866));
#33191=CARTESIAN_POINT('Ctrl Pts',(0.0898865489335327,0.106333191146418,
0.214478731343283));
#33192=CARTESIAN_POINT('Ctrl Pts',(-0.0406746665030564,0.133161220808791,
0.222422388059702));
#33193=CARTESIAN_POINT('Ctrl Pts',(-0.133960919120719,0.0379580211457631,
0.230366044776119));
#33194=CARTESIAN_POINT('Ctrl Pts',(-0.104483085165326,-0.0920305608755558,
0.238309701492537));
#33195=CARTESIAN_POINT('Ctrl Pts',(0.0207448421498254,-0.137680756627218,
0.246253358208955));
#33196=CARTESIAN_POINT('Ctrl Pts',(0.126961839902422,-0.0571579428392388,
0.254197014925373));
#33197=CARTESIAN_POINT('Ctrl Pts',(0.116828827462796,0.075745391244066,
0.262140671641791));
#33198=CARTESIAN_POINT('Ctrl Pts',(-0.000368128572008151,0.139234348141551,
0.270084328358209));
#33199=CARTESIAN_POINT('Ctrl Pts',(-0.117227725261659,0.0751265575612168,
0.278027985074627));
#33200=CARTESIAN_POINT('Ctrl Pts',(-0.12665782156486,-0.0578285003930446,
0.285971641791045));
#33201=CARTESIAN_POINT('Ctrl Pts',(-0.0200165152988323,-0.137788527592198,
0.293915298507463));
#33202=CARTESIAN_POINT('Ctrl Pts',(0.104968269293632,-0.0914767820950745,
0.301858955223881));
#33203=CARTESIAN_POINT('Ctrl Pts',(0.133758329466478,0.0386658573002006,
0.309802611940298));
#33204=CARTESIAN_POINT('Ctrl Pts',(0.0399699596916912,0.133374441107753,
0.317746268656717));
#33205=CARTESIAN_POINT('Ctrl Pts',(-0.0904475674556682,0.10585639689043,
0.325689925373134));
#33206=CARTESIAN_POINT('Ctrl Pts',(-0.137977390731318,-0.0186702671811566,
0.333633582089553));
#33207=CARTESIAN_POINT('Ctrl Pts',(-0.0590623637863932,-0.126087177724698,
0.34157723880597));
#33208=CARTESIAN_POINT('Ctrl Pts',(0.0739784273282333,-0.117955633685244,
0.349520895522388));
#33209=CARTESIAN_POINT('Ctrl Pts',(0.139224117680559,-0.00172752115601949,
0.357464552238807));
#33210=CARTESIAN_POINT('Ctrl Pts',(0.0768824352591712,0.11608372080921,
0.365408208955224));
#33211=CARTESIAN_POINT('Ctrl Pts',(-0.0559156297430559,0.12751384888047,
0.373351865671643));
#33212=CARTESIAN_POINT('Ctrl Pts',(-0.137471653907146,0.0220880940313751,
0.381295522388059));
#33213=CARTESIAN_POINT('Ctrl Pts',(-0.0930462892870504,-0.103579565247593,
0.389239179104478));
#33214=CARTESIAN_POINT('Ctrl Pts',(0.0366482838797405,-0.134325140358292,
0.397182835820896));
#33215=CARTESIAN_POINT('Ctrl Pts',(0.132757756905765,-0.0419728350502109,
0.405126492537314));
#33216=CARTESIAN_POINT('Ctrl Pts',(0.107205710503746,0.0888440680441954,
0.413070149253731));
#33217=CARTESIAN_POINT('Ctrl Pts',(-0.0165914302528927,0.138242796692368,
0.42101380597015));
#33218=CARTESIAN_POINT('Ctrl Pts',(-0.125184012727194,0.0609533479579989,
0.428957462686568));
#33219=CARTESIAN_POINT('Ctrl Pts',(-0.119055601044071,-0.0721945965608292,
0.436901119402986));
#33220=CARTESIAN_POINT('Ctrl Pts',(-0.00382300141363195,-0.139182551176009,
0.444844776119403));
#33221=CARTESIAN_POINT('Ctrl Pts',(0.11491384000461,-0.0786205074584852,
0.452788432835821));
#33222=CARTESIAN_POINT('Ctrl Pts',(0.128340187352459,0.0539893538840985,
0.460732089552239));
#33223=CARTESIAN_POINT('Ctrl Pts',(0.024156191824071,0.137125039167645,
0.468675746268657));
#33224=CARTESIAN_POINT('Ctrl Pts',(-0.102170290252407,0.094592052461424,
0.476619402985075));
#33225=CARTESIAN_POINT('Ctrl Pts',(-0.13485601995589,-0.0346173432617789,
0.484563059701493));
#33226=CARTESIAN_POINT('Ctrl Pts',(-0.0439766578214066,-0.132120623957634,
0.492506716417911));
#33227=CARTESIAN_POINT('Ctrl Pts',(0.087240331747497,-0.108512430051717,
0.500450373134329));
#33228=CARTESIAN_POINT('Ctrl Pts',(0.138438921804208,0.0144739368962113,
0.508394029850746));
#33229=CARTESIAN_POINT('Ctrl Pts',(0.0629040591690992,0.12431971381125,
0.516337686567165));
#33230=CARTESIAN_POINT('Ctrl Pts',(-0.0705459363093062,0.119993110375402,
0.524281343283582));
#33231=CARTESIAN_POINT('Ctrl Pts',(-0.116003159314893,0.0441585924901374,
0.529577114427861));
#33232=CARTESIAN_POINT('Ctrl Pts',(-0.117668597464311,0.00500517689817385,
0.532225));
#33233=CARTESIAN_POINT('',(0.0684664424539457,-0.0958295198918399,0.));
#33234=CARTESIAN_POINT('Ctrl Pts',(0.0684664424539458,-0.0958295198918399,
-1.2490009027033E-16));
#33235=CARTESIAN_POINT('Ctrl Pts',(0.100353055357967,-0.0730477825951437,
0.00264788557213918));
#33236=CARTESIAN_POINT('Ctrl Pts',(0.139044776673305,0.00645180185613777,
0.00794365671641779));
#33237=CARTESIAN_POINT('Ctrl Pts',(0.0697747251423586,0.120597676732883,
0.0158873134328358));
#33238=CARTESIAN_POINT('Ctrl Pts',(-0.0634953696301243,0.123867541975778,
0.0238309701492536));
#33239=CARTESIAN_POINT('Ctrl Pts',(-0.116013612970437,0.0468487789511056,
0.0293896285137698));
#33240=CARTESIAN_POINT('Ctrl Pts',(-0.117946226519694,0.00395164958315818,
0.0323004013061468));
#33241=CARTESIAN_POINT('Ctrl Pts',(-0.117919967015755,7.48285734863559E-5,
0.0325632885263843));
#33242=CARTESIAN_POINT('Ctrl Pts',(0.0635548502597316,0.132093933345895,
7.26415455565288E-18));
#33243=CARTESIAN_POINT('Ctrl Pts',(0.0667625318922158,0.13018322972067,
8.97431508554919E-18));
#33244=CARTESIAN_POINT('Ctrl Pts',(0.0698866263065284,0.128144700630429,
-1.82766240468292E-17));
#33245=CARTESIAN_POINT('Ctrl Pts',(0.0729183991770622,0.125977863427922,
-1.55040910665427E-17));
#33246=CARTESIAN_POINT('Ctrl Pts',(0.0787736058599248,0.121793090949712,
-9.35723626730848E-18));
#33247=CARTESIAN_POINT('Ctrl Pts',(0.0842851176408076,0.117130107773036,
-2.42858544627756E-17));
#33248=CARTESIAN_POINT('Ctrl Pts',(0.0894225077026563,0.112048986470911,
-3.0140820395097E-17));
#33249=CARTESIAN_POINT('Ctrl Pts',(0.0927550575340165,0.108752937361409,
-3.39388512036349E-17));
#33250=CARTESIAN_POINT('Ctrl Pts',(0.095930929613759,0.105278801629612,
-4.52445550988079E-17));
#33251=CARTESIAN_POINT('Ctrl Pts',(0.0989262797420343,0.101660133512415,
-3.46944695195361E-17));
#33252=CARTESIAN_POINT('Ctrl Pts',(0.103069367071931,0.0966548895891983,
-2.01018763264428E-17));
#33253=CARTESIAN_POINT('Ctrl Pts',(0.106874603061403,0.0913668016366946,
-3.77038544403596E-17));
#33254=CARTESIAN_POINT('Ctrl Pts',(0.110317478847291,0.0858396385675292,
-3.33934269125535E-17));
#33255=CARTESIAN_POINT('Ctrl Pts',(0.112268215177796,0.082707943300496,
-3.09511350317464E-17));
#33256=CARTESIAN_POINT('Ctrl Pts',(0.114103333501928,0.079497785539906,
-4.97099315558713E-17));
#33257=CARTESIAN_POINT('Ctrl Pts',(0.115814486180912,0.0762220963964089,
-4.59701721133854E-17));
#33258=CARTESIAN_POINT('Ctrl Pts',(0.120425861906472,0.0673944601566279,
-3.58919154362862E-17));
#33259=CARTESIAN_POINT('Ctrl Pts',(0.124112940735196,0.0581470311761757,
-7.4029188042833E-18));
#33260=CARTESIAN_POINT('Ctrl Pts',(0.126786742395323,0.0486381528803429,
-1.99493199737333E-17));
#33261=CARTESIAN_POINT('Ctrl Pts',(0.128289456800478,0.0432940285927791,
-2.70005751402403E-17));
#33262=CARTESIAN_POINT('Ctrl Pts',(0.129471235246761,0.0378670663167402,
-8.81130640021771E-18));
#33263=CARTESIAN_POINT('Ctrl Pts',(0.130308765287913,0.0323855967712197,
-1.47451495458029E-17));
#33264=CARTESIAN_POINT('Ctrl Pts',(0.130909407220836,0.0284545133457784,
-1.90006566219738E-17));
#33265=CARTESIAN_POINT('Ctrl Pts',(0.131332629221345,0.0244917931761562,
-4.99383881545994E-18));
#33266=CARTESIAN_POINT('Ctrl Pts',(0.1315678106143,0.0205341495544984,-6.07153216591882E-18));
#33267=CARTESIAN_POINT('Ctrl Pts',(0.131851015138327,0.015768370408227,
-7.36928633144951E-18));
#33268=CARTESIAN_POINT('Ctrl Pts',(0.131863254926577,0.0110027231344166,
-1.87693227394301E-17));
#33269=CARTESIAN_POINT('Ctrl Pts',(0.131591710623677,0.00625556877829329,
-1.38777878078145E-17));
#33270=CARTESIAN_POINT('Ctrl Pts',(0.131146495407245,-0.00152771126671145,
-5.8577860622257E-18));
#33271=CARTESIAN_POINT('Ctrl Pts',(0.12993932260643,-0.00926206422336292,
-1.85374582714576E-17));
#33272=CARTESIAN_POINT('Ctrl Pts',(0.128016835267175,-0.0168585737917118,
-1.04083408558608E-17));
#33273=CARTESIAN_POINT('Ctrl Pts',(0.126984115402176,-0.0209392593575938,
-6.04154952851233E-18));
#33274=CARTESIAN_POINT('Ctrl Pts',(0.125742427413826,-0.0249846391579523,
1.89772622437785E-17));
#33275=CARTESIAN_POINT('Ctrl Pts',(0.124308621487175,-0.0289511201777135,
1.38777878078145E-17));
#33276=CARTESIAN_POINT('Ctrl Pts',(0.121785637190381,-0.0359307044717815,
4.90454136999372E-18));
#33277=CARTESIAN_POINT('Ctrl Pts',(0.118666317325564,-0.042682712152767,
2.07260850608487E-18));
#33278=CARTESIAN_POINT('Ctrl Pts',(0.114994151346376,-0.0491304207397526,
8.67361737988404E-18));
#33279=CARTESIAN_POINT('Ctrl Pts',(0.112470213235982,-0.0535620334499726,
1.32105958166033E-17));
#33280=CARTESIAN_POINT('Ctrl Pts',(0.109684704250007,-0.0578497076893306,
-2.69424258846107E-17));
#33281=CARTESIAN_POINT('Ctrl Pts',(0.106648013733876,-0.0619641182107045,
-2.60208521396521E-17));
#33282=CARTESIAN_POINT('Ctrl Pts',(0.104460102807982,-0.0649285176730499,
-2.53568657192706E-17));
#33283=CARTESIAN_POINT('Ctrl Pts',(0.102139560475227,-0.0678046962501359,
-1.87244270863087E-17));
#33284=CARTESIAN_POINT('Ctrl Pts',(0.0997061632112326,-0.0705633954799611,
-1.90819582357449E-17));
#33285=CARTESIAN_POINT('Ctrl Pts',(0.0939222145804643,-0.0771205552455056,
-1.9931775005426E-17));
#33286=CARTESIAN_POINT('Ctrl Pts',(0.087486631308301,-0.0830406987797476,
-2.77894727952103E-19));
#33287=CARTESIAN_POINT('Ctrl Pts',(0.0804584136226653,-0.0881761753022089,
-1.73472347597681E-18));
#33288=CARTESIAN_POINT('Ctrl Pts',(0.0766344364937381,-0.0909703324621629,
-2.52736822068868E-18));
#33289=CARTESIAN_POINT('Ctrl Pts',(0.0726345968903183,-0.0935314830199203,
-1.19936303452846E-17));
#33290=CARTESIAN_POINT('Ctrl Pts',(0.0684664424539472,-0.0958295198918389,
-1.04083408558608E-17));
#33291=CARTESIAN_POINT('Ctrl Pts',(-0.00157033164522019,0.146071601053478,
0.50365));
#33292=CARTESIAN_POINT('Ctrl Pts',(0.0218930565124332,0.146360870028846,
0.502379967541691));
#33293=CARTESIAN_POINT('Ctrl Pts',(0.0454120282149095,0.141318853716995,
0.501109935083381));
#33294=CARTESIAN_POINT('Ctrl Pts',(0.0661716191392787,0.130837066204352,
0.499839902625071));
#33295=CARTESIAN_POINT('Ctrl Pts',(0.109453206891224,0.108983629511958,
0.497192017052932));
#33296=CARTESIAN_POINT('Ctrl Pts',(0.140740342380216,0.0634846428806245,
0.494544131480792));
#33297=CARTESIAN_POINT('Ctrl Pts',(0.145780480343632,0.0152641882646972,
0.491896245908653));
#33298=CARTESIAN_POINT('Ctrl Pts',(0.150820618307048,-0.0329562663512301,
0.489248360336514));
#33299=CARTESIAN_POINT('Ctrl Pts',(0.129613758744889,-0.0838981889517511,
0.486600474764375));
#33300=CARTESIAN_POINT('Ctrl Pts',(0.0918347732807851,-0.114258500252904,
0.483952589192235));
#33301=CARTESIAN_POINT('Ctrl Pts',(0.0540557878166811,-0.144618811554058,
0.481304703620096));
#33302=CARTESIAN_POINT('Ctrl Pts',(-0.000295323549367926,-0.154397511555843,
0.478656818047957));
#33303=CARTESIAN_POINT('Ctrl Pts',(-0.0462923532978867,-0.139093547851452,
0.476008932475817));
#33304=CARTESIAN_POINT('Ctrl Pts',(-0.0922893830464049,-0.123789584147061,
0.473361046903678));
#33305=CARTESIAN_POINT('Ctrl Pts',(-0.129932331177393,-0.0834029567364939,
0.470713161331538));
#33306=CARTESIAN_POINT('Ctrl Pts',(-0.141984461802563,-0.0364498679458208,
0.468065275759399));
#33307=CARTESIAN_POINT('Ctrl Pts',(-0.145018518318758,-0.0246296902999453,
0.467398685367696));
#33308=CARTESIAN_POINT('Ctrl Pts',(-0.146430750426956,-0.0123933615350992,
0.466732094975993));
#33309=CARTESIAN_POINT('Ctrl Pts',(-0.146320034481408,-0.000132042578932776,
0.466065504584291));
#33310=CARTESIAN_POINT('Origin',(0.,0.,-0.0924367114736154));
#33311=CARTESIAN_POINT('',(-0.0684664424539447,-0.0958295198918406,0.));
#33312=CARTESIAN_POINT('Ctrl Pts',(-0.0686153921261821,-0.095961513397809,
-8.6871699070401E-17));
#33313=CARTESIAN_POINT('Ctrl Pts',(-0.0390777571216276,-0.11683521110507,
0.00245324280107157));
#33314=CARTESIAN_POINT('Ctrl Pts',(0.0440758903380829,-0.130444567971902,
0.00755732030717748));
#33315=CARTESIAN_POINT('Ctrl Pts',(0.134343829836486,-0.03677094505856,
0.0153122325183177));
#33316=CARTESIAN_POINT('Ctrl Pts',(0.103577487134497,0.0931457228401511,
0.0232647366334205));
#33317=CARTESIAN_POINT('Ctrl Pts',(-0.022319455813322,0.137480661654608,
0.0312172407485234));
#33318=CARTESIAN_POINT('Ctrl Pts',(-0.107013184840641,0.0716760847082379,
0.0376078990285884));
#33319=CARTESIAN_POINT('Ctrl Pts',(-0.117673522927843,0.0162276125558733,
0.0413477226036194));
#33320=CARTESIAN_POINT('Ctrl Pts',(-0.117605093279175,5.6374090473453E-5,
0.042436711473616));
#33321=CARTESIAN_POINT('Origin',(0.,0.,0.));
#33322=CARTESIAN_POINT('Ctrl Pts',(-0.0510216505388437,0.106149619882937,
-0.0164977839420935));
#33323=CARTESIAN_POINT('Ctrl Pts',(-0.0863815445949669,0.0891536084077042,
-0.0138469492370593));
#33324=CARTESIAN_POINT('Ctrl Pts',(-0.138162556478479,0.0173380738482791,
-0.00854527982699074));
#33325=CARTESIAN_POINT('Ctrl Pts',(-0.0892152289856901,-0.107087400898305,
-0.000592775711887911));
#33326=CARTESIAN_POINT('Ctrl Pts',(0.0417759011768067,-0.132831332515275,
0.00735972840321487));
#33327=CARTESIAN_POINT('Ctrl Pts',(0.134343829836486,-0.03677094505856,
0.0153122325183177));
#33328=CARTESIAN_POINT('Ctrl Pts',(0.103577487134497,0.0931457228401511,
0.0232647366334205));
#33329=CARTESIAN_POINT('Ctrl Pts',(-0.022319455813322,0.137480661654608,
0.0312172407485234));
#33330=CARTESIAN_POINT('Ctrl Pts',(-0.127711920735776,0.0555937658099327,
0.0391697448636261));
#33331=CARTESIAN_POINT('Ctrl Pts',(-0.115832853027164,-0.0773572203301017,
0.047122248978729));
#33332=CARTESIAN_POINT('Ctrl Pts',(0.00241643506700816,-0.139265216174241,
0.0550747530938317));
#33333=CARTESIAN_POINT('Ctrl Pts',(0.118445458723555,-0.0732914200146354,
0.0630272572089346));
#33334=CARTESIAN_POINT('Ctrl Pts',(0.125708256673902,0.0599868231457294,
0.0709797613240373));
#33335=CARTESIAN_POINT('Ctrl Pts',(0.0175344664057042,0.138178956948752,
0.0789322654391402));
#33336=CARTESIAN_POINT('Ctrl Pts',(-0.106740805893122,0.0894837054538652,
0.0868847695542431));
#33337=CARTESIAN_POINT('Ctrl Pts',(-0.132997503503664,-0.0413835288220579,
0.0948372736693457));
#33338=CARTESIAN_POINT('Ctrl Pts',(-0.0371242974264225,-0.134248668971966,
0.102789777784449));
#33339=CARTESIAN_POINT('Ctrl Pts',(0.0928396337021713,-0.10383510521762,
0.110742281899551));
#33340=CARTESIAN_POINT('Ctrl Pts',(0.137550169005636,0.0219289054269618,
0.118694786014654));
#33341=CARTESIAN_POINT('Ctrl Pts',(0.0559501922162531,0.127555870431356,
0.126647290129757));
#33342=CARTESIAN_POINT('Ctrl Pts',(-0.0770281035821754,0.116049974518826,
0.13459979424486));
#33343=CARTESIAN_POINT('Ctrl Pts',(-0.13927251071013,-0.00202308703008076,
0.142552298359963));
#33344=CARTESIAN_POINT('Ctrl Pts',(-0.0736248085349355,-0.118238371369349,
0.150504802475065));
#33345=CARTESIAN_POINT('Ctrl Pts',(0.0596315829014974,-0.125876921640408,
0.158457306590168));
#33346=CARTESIAN_POINT('Ctrl Pts',(0.138129079193178,-0.0179243554725553,
0.166409810705271));
#33347=CARTESIAN_POINT('Ctrl Pts',(0.0897844651888838,0.106487909275724,
0.174362314820374));
#33348=CARTESIAN_POINT('Ctrl Pts',(-0.0410080379701501,0.133113732800722,
0.182314818935477));
#33349=CARTESIAN_POINT('Ctrl Pts',(-0.134143401206605,0.0375029724551737,
0.190267323050579));
#33350=CARTESIAN_POINT('Ctrl Pts',(-0.104096649768354,-0.0925462723956308,
0.198219827165683));
#33351=CARTESIAN_POINT('Ctrl Pts',(0.0215406810767683,-0.137611496939632,
0.206172331280785));
#33352=CARTESIAN_POINT('Ctrl Pts',(0.127397488829925,-0.056309900280862,
0.214124835395888));
#33353=CARTESIAN_POINT('Ctrl Pts',(0.116266864218555,0.0767003345124148,
0.222077339510991));
#33354=CARTESIAN_POINT('Ctrl Pts',(-0.0016300870944122,0.139277664563073,
0.230029843626094));
#33355=CARTESIAN_POINT('Ctrl Pts',(-0.1180301509465,0.0739581536911037,
0.237982347741196));
#33356=CARTESIAN_POINT('Ctrl Pts',(-0.126044685167542,-0.0592761534753867,
0.245934851856299));
#33357=CARTESIAN_POINT('Ctrl Pts',(-0.0183140487741412,-0.138077951344142,
0.253887355971402));
#33358=CARTESIAN_POINT('Ctrl Pts',(0.106234136865658,-0.0900845891054932,
0.261839860086505));
#33359=CARTESIAN_POINT('Ctrl Pts',(0.133228916899009,0.040632262203075,
0.269792364201608));
#33360=CARTESIAN_POINT('Ctrl Pts',(0.0378813411502606,0.134037043471229,
0.27774486831671));
#33361=CARTESIAN_POINT('Ctrl Pts',(-0.092252170148986,0.104357376993109,
0.285697372431813));
#33362=CARTESIAN_POINT('Ctrl Pts',(-0.137671731315388,-0.021152291274371,
0.293649876546916));
#33363=CARTESIAN_POINT('Ctrl Pts',(-0.0566691588697243,-0.127238089669758,
0.301602380662019));
#33364=CARTESIAN_POINT('Ctrl Pts',(0.0763719541489209,-0.116482829853556,
0.309554884777122));
#33365=CARTESIAN_POINT('Ctrl Pts',(0.139281709756163,0.00123707506708643,
0.317507388892225));
#33366=CARTESIAN_POINT('Ctrl Pts',(0.0742909098282569,0.117820990265484,
0.325459893007327));
#33367=CARTESIAN_POINT('Ctrl Pts',(-0.0589202520252667,0.1262114453589,
0.33341239712243));
#33368=CARTESIAN_POINT('Ctrl Pts',(-0.13802572406761,0.0187035960922139,
0.341364901237533));
#33369=CARTESIAN_POINT('Ctrl Pts',(-0.0903839958430062,-0.105979518461414,
0.349317405352636));
#33370=CARTESIAN_POINT('Ctrl Pts',(0.0402561631274929,-0.133343040355529,
0.357269909467738));
#33371=CARTESIAN_POINT('Ctrl Pts',(0.133929618074243,-0.0382594079720193,
0.365222413582842));
#33372=CARTESIAN_POINT('Ctrl Pts',(0.104617274119081,0.0919573329132998,
0.373174917697944));
#33373=CARTESIAN_POINT('Ctrl Pts',(-0.020763734615072,0.137730870367254,
0.381127421813047));
#33374=CARTESIAN_POINT('Ctrl Pts',(-0.127077674436729,0.0570279646339328,
0.38907992592815));
#33375=CARTESIAN_POINT('Ctrl Pts',(-0.116697873675526,-0.0760429626350431,
0.397032430043252));
#33376=CARTESIAN_POINT('Ctrl Pts',(0.000844063931402275,-0.139284651766041,
0.404984934158356));
#33377=CARTESIAN_POINT('Ctrl Pts',(0.117610871049501,-0.0746230633995127,
0.412937438273457));
#33378=CARTESIAN_POINT('Ctrl Pts',(0.126377239427685,0.0585638604483229,
0.420889942388562));
#33379=CARTESIAN_POINT('Ctrl Pts',(0.0190929207373193,0.137972437690235,
0.428842446503664));
#33380=CARTESIAN_POINT('Ctrl Pts',(-0.105723916050958,0.0906826070998613,
0.436794950618767));
#33381=CARTESIAN_POINT('Ctrl Pts',(-0.133456368516637,-0.0398795994144927,
0.44474745473387));
#33382=CARTESIAN_POINT('Ctrl Pts',(-0.038636663810782,-0.133821400192823,
0.452699958848972));
#33383=CARTESIAN_POINT('Ctrl Pts',(0.0916608011058181,-0.104875817685159,
0.460652462964076));
#33384=CARTESIAN_POINT('Ctrl Pts',(0.137790741908166,0.0203740232160909,
0.468604967079177));
#33385=CARTESIAN_POINT('Ctrl Pts',(0.0573828398023632,0.126918127906013,
0.476557471194281));
#33386=CARTESIAN_POINT('Ctrl Pts',(-0.0757067578384881,0.11690841395886,
0.484509975309383));
#33387=CARTESIAN_POINT('Ctrl Pts',(-0.139299045817393,-0.000444250914572553,
0.492462479424487));
#33388=CARTESIAN_POINT('Ctrl Pts',(-0.0749307309976486,-0.117412744486246,
0.500414983539588));
#33389=CARTESIAN_POINT('Ctrl Pts',(0.0581614397283287,-0.126517333775439,
0.508367487654693));
#33390=CARTESIAN_POINT('Ctrl Pts',(0.138005962114904,-0.01953005209576,
0.516319991769794));
#33391=CARTESIAN_POINT('Ctrl Pts',(0.0908022345067483,0.105567300931769,
0.524272495884898));
#33392=CARTESIAN_POINT('Ctrl Pts',(0.00421962447768953,0.124065836989857,
0.529574165294966));
#33393=CARTESIAN_POINT('Ctrl Pts',(-0.0334019664626881,0.11293918390632,
0.532225));
#33394=CARTESIAN_POINT('Ctrl Pts',(-0.0551480035117362,0.114734422509853,
-0.0109985226280624));
#33395=CARTESIAN_POINT('Ctrl Pts',(-0.0933676130497917,0.096363866272985,
-0.0083476879230281));
#33396=CARTESIAN_POINT('Ctrl Pts',(-0.149336390912421,0.0187402827500406,
-0.00304601851295955));
#33397=CARTESIAN_POINT('Ctrl Pts',(-0.0964304703874203,-0.115748046141832,
0.00490648560214325));
#33398=CARTESIAN_POINT('Ctrl Pts',(0.0451545083405425,-0.143574006615959,
0.0128589897172461));
#33399=CARTESIAN_POINT('Ctrl Pts',(0.145208826475777,-0.0397447786538297,
0.0208114938323489));
#33400=CARTESIAN_POINT('Ctrl Pts',(0.1119542696856,0.100678841159424,0.0287639979474517));
#33401=CARTESIAN_POINT('Ctrl Pts',(-0.0241245317345429,0.148599348152253,
0.0367165020625545));
#33402=CARTESIAN_POINT('Ctrl Pts',(-0.138040564718016,0.060089886543023,
0.0446690061776573));
#33403=CARTESIAN_POINT('Ctrl Pts',(-0.125200782766784,-0.0836134506306251,
0.0526215102927601));
#33404=CARTESIAN_POINT('Ctrl Pts',(0.00261186316306541,-0.150528227713698,
0.0605740144078629));
#33405=CARTESIAN_POINT('Ctrl Pts',(0.128024681770397,-0.0792188305486153,
0.0685265185229658));
#33406=CARTESIAN_POINT('Ctrl Pts',(0.135874855228935,0.0648382304092657,
0.0764790226380685));
#33407=CARTESIAN_POINT('Ctrl Pts',(0.0189525584669602,0.149354117763329,
0.0844315267531714));
#33408=CARTESIAN_POINT('Ctrl Pts',(-0.115373420421943,0.096720659768857,
0.0923840308682741));
#33409=CARTESIAN_POINT('Ctrl Pts',(-0.143753616608078,-0.0447304030485916,
0.100336534983377));
#33410=CARTESIAN_POINT('Ctrl Pts',(-0.0401267082350556,-0.145105969519263,
0.10828903909848));
#33411=CARTESIAN_POINT('Ctrl Pts',(0.100347997200478,-0.112232722514991,
0.116241543213583));
#33412=CARTESIAN_POINT('Ctrl Pts',(0.148674476878943,0.0237023957618521,
0.124194047328685));
#33413=CARTESIAN_POINT('Ctrl Pts',(0.0604751387741805,0.137871893915615,
0.132146551443788));
#33414=CARTESIAN_POINT('Ctrl Pts',(-0.0832577167141655,0.125435463861147,
0.140099055558891));
#33415=CARTESIAN_POINT('Ctrl Pts',(-0.150536112191887,-0.00218670328107987,
0.148051559673994));
#33416=CARTESIAN_POINT('Ctrl Pts',(-0.0795791817151125,-0.127800846319831,
0.156004063789097));
#33417=CARTESIAN_POINT('Ctrl Pts',(0.0644542602705204,-0.136057160898527,
0.163956567904199));
#33418=CARTESIAN_POINT('Ctrl Pts',(0.149300206166772,-0.0193739796362248,
0.171909072019302));
#33419=CARTESIAN_POINT('Ctrl Pts',(0.0970457433117808,0.115100070904688,
0.179861576134405));
#33420=CARTESIAN_POINT('Ctrl Pts',(-0.0443245445434091,0.143879245897109,
0.187814080249508));
#33421=CARTESIAN_POINT('Ctrl Pts',(-0.144992188270862,0.0405360084359473,
0.195766584364611));
#33422=CARTESIAN_POINT('Ctrl Pts',(-0.11251541936329,-0.100030910430598,
0.203719088479714));
#33423=CARTESIAN_POINT('Ctrl Pts',(0.023282773942454,-0.148740764681937,
0.211671592594816));
#33424=CARTESIAN_POINT('Ctrl Pts',(0.13770070327361,-0.0608639380662604,
0.219624096709919));
#33425=CARTESIAN_POINT('Ctrl Pts',(0.125669894417509,0.0829034394687354,
0.227576600825022));
#33426=CARTESIAN_POINT('Ctrl Pts',(-0.00176191965288545,0.150541682860363,
0.235529104940125));
#33427=CARTESIAN_POINT('Ctrl Pts',(-0.127575786164206,0.0799394860104231,
0.243481609055227));
#33428=CARTESIAN_POINT('Ctrl Pts',(-0.136238492225245,-0.0640700856498972,
0.25143411317033));
#33429=CARTESIAN_POINT('Ctrl Pts',(-0.0197951892077968,-0.149244943376008,
0.259386617285433));
#33430=CARTESIAN_POINT('Ctrl Pts',(0.114825774765427,-0.0973701396147685,
0.267339121400536));
#33431=CARTESIAN_POINT('Ctrl Pts',(0.144003745457388,0.0439183780806738,
0.275291625515639));
#33432=CARTESIAN_POINT('Ctrl Pts',(0.0409449775285778,0.144877228901612,
0.283244129630741));
#33433=CARTESIAN_POINT('Ctrl Pts',(-0.0997130227974173,0.112797232784741,
0.291196633745845));
#33434=CARTESIAN_POINT('Ctrl Pts',(-0.148805870485663,-0.0228629732899794,
0.299149137860947));
#33435=CARTESIAN_POINT('Ctrl Pts',(-0.0612522515314454,-0.137528412778265,
0.30710164197605));
#33436=CARTESIAN_POINT('Ctrl Pts',(0.0825485014914671,-0.125903326175825,
0.315054146091153));
#33437=CARTESIAN_POINT('Ctrl Pts',(0.150546055206619,0.00133712295512629,
0.323006650206255));
#33438=CARTESIAN_POINT('Ctrl Pts',(0.0802991536500716,0.12734970970746,
0.330959154321359));
#33439=CARTESIAN_POINT('Ctrl Pts',(-0.0636854008305359,0.136418739071857,
0.338911658436461));
#33440=CARTESIAN_POINT('Ctrl Pts',(-0.149188492242044,0.0202162409895048,
0.346864162551565));
#33441=CARTESIAN_POINT('Ctrl Pts',(-0.0976937607371238,-0.114550564212591,
0.354816666666667));
#33442=CARTESIAN_POINT('Ctrl Pts',(0.0435118621620017,-0.144127098596976,
0.36276917078177));
#33443=CARTESIAN_POINT('Ctrl Pts',(0.144761115524102,-0.041353620334011,
0.370721674896872));
#33444=CARTESIAN_POINT('Ctrl Pts',(0.113078148973544,0.0993943407332879,
0.378674179011976));
#33445=CARTESIAN_POINT('Ctrl Pts',(-0.0224429922861266,0.148869792381672,
0.386626683127078));
#33446=CARTESIAN_POINT('Ctrl Pts',(-0.137355024035624,0.0616400755499871,
0.394579187242181));
#33447=CARTESIAN_POINT('Ctrl Pts',(-0.126135761569897,-0.0821929029373033,
0.402531691357283));
#33448=CARTESIAN_POINT('Ctrl Pts',(0.000912327221120078,-0.150549235150219,
0.410484195472387));
#33449=CARTESIAN_POINT('Ctrl Pts',(0.127122597194663,-0.0806581699915775,
0.418436699587489));
#33450=CARTESIAN_POINT('Ctrl Pts',(0.136597941661171,0.0633001862455649,
0.426389203702593));
#33451=CARTESIAN_POINT('Ctrl Pts',(0.0206370520896696,0.149130896352934,
0.434341707817695));
#33452=CARTESIAN_POINT('Ctrl Pts',(-0.114274290072485,0.0980165220446819,
0.442294211932798));
#33453=CARTESIAN_POINT('Ctrl Pts',(-0.144249592121994,-0.0431048440285699,
0.450246716047901));
#33454=CARTESIAN_POINT('Ctrl Pts',(-0.0417613865685641,-0.144644145570336,
0.458199220163003));
#33455=CARTESIAN_POINT('Ctrl Pts',(0.0990738270496334,-0.113357602133906,
0.466151724278107));
#33456=CARTESIAN_POINT('Ctrl Pts',(0.148934506006449,0.0220217631535408,
0.474104228393209));
#33457=CARTESIAN_POINT('Ctrl Pts',(0.0620236510875902,0.137182574251203,
0.482056732508312));
#33458=CARTESIAN_POINT('Ctrl Pts',(-0.0818295077294796,0.126363329203676,
0.490009236623415));
#33459=CARTESIAN_POINT('Ctrl Pts',(-0.150564793313981,-0.000480179506898605,
0.497961740738518));
#33460=CARTESIAN_POINT('Ctrl Pts',(-0.0809907200679325,-0.126908447234973,
0.50591424485362));
#33461=CARTESIAN_POINT('Ctrl Pts',(0.0628652199313619,-0.136749366076106,
0.513866748968723));
#33462=CARTESIAN_POINT('Ctrl Pts',(0.149167132050327,-0.0211095362495466,
0.521819253083827));
#33463=CARTESIAN_POINT('Ctrl Pts',(0.0981458242641405,0.114105008776176,
0.529771757198928));
#33464=CARTESIAN_POINT('Ctrl Pts',(0.00456088470396912,0.134099605593792,
0.535073426608997));
#33465=CARTESIAN_POINT('Ctrl Pts',(-0.0361033354336669,0.122073089461044,
0.537724261314032));
#33466=CARTESIAN_POINT('Ctrl Pts',(-0.0592743564846287,0.123319225136769,
-0.00549926131403118));
#33467=CARTESIAN_POINT('Ctrl Pts',(-0.100353681504617,0.103574124138266,
-0.00284842660899691));
#33468=CARTESIAN_POINT('Ctrl Pts',(-0.160510225346362,0.0201424916518021,
0.00245324280107164));
#33469=CARTESIAN_POINT('Ctrl Pts',(-0.103645711789151,-0.124408691385358,
0.0104057469161744));
#33470=CARTESIAN_POINT('Ctrl Pts',(0.0485331155042784,-0.154316680716642,
0.0183582510312773));
#33471=CARTESIAN_POINT('Ctrl Pts',(0.156073823115068,-0.0427186122490994,
0.02631075514638));
#33472=CARTESIAN_POINT('Ctrl Pts',(0.120331052236703,0.108211959478697,
0.0342632592614829));
#33473=CARTESIAN_POINT('Ctrl Pts',(-0.0259296076557639,0.159718034649898,
0.0422157633765857));
#33474=CARTESIAN_POINT('Ctrl Pts',(-0.148369208700255,0.0645860072761131,
0.0501682674916885));
#33475=CARTESIAN_POINT('Ctrl Pts',(-0.134568712506405,-0.0898696809311483,
0.0581207716067913));
#33476=CARTESIAN_POINT('Ctrl Pts',(0.00280729125912282,-0.161791239253156,
0.0660732757218941));
#33477=CARTESIAN_POINT('Ctrl Pts',(0.137603904817239,-0.0851462410825952,
0.074025779836997));
#33478=CARTESIAN_POINT('Ctrl Pts',(0.146041453783967,0.0696896376728019,
0.0819782839520996));
#33479=CARTESIAN_POINT('Ctrl Pts',(0.0203706505282163,0.160529278577907,
0.0899307880672026));
#33480=CARTESIAN_POINT('Ctrl Pts',(-0.124006034950765,0.103957614083849,
0.0978832921823053));
#33481=CARTESIAN_POINT('Ctrl Pts',(-0.154509729712493,-0.0480772772751253,
0.105835796297408));
#33482=CARTESIAN_POINT('Ctrl Pts',(-0.0431291190436888,-0.155963270066561,
0.113788300412511));
#33483=CARTESIAN_POINT('Ctrl Pts',(0.107856360698785,-0.120630339812362,
0.121740804527614));
#33484=CARTESIAN_POINT('Ctrl Pts',(0.159798784752249,0.0254758860967424,
0.129693308642717));
#33485=CARTESIAN_POINT('Ctrl Pts',(0.065000085332108,0.148187917399874,
0.137645812757819));
#33486=CARTESIAN_POINT('Ctrl Pts',(-0.0894873298461556,0.134820953203468,
0.145598316872922));
#33487=CARTESIAN_POINT('Ctrl Pts',(-0.161799713673645,-0.00235031953207901,
0.153550820988025));
#33488=CARTESIAN_POINT('Ctrl Pts',(-0.0855335548952896,-0.137363321270313,
0.161503325103128));
#33489=CARTESIAN_POINT('Ctrl Pts',(0.0692769376395434,-0.146237400156646,
0.169455829218231));
#33490=CARTESIAN_POINT('Ctrl Pts',(0.160471333140366,-0.0208236037998943,
0.177408333333334));
#33491=CARTESIAN_POINT('Ctrl Pts',(0.104307021434678,0.123712232533651,
0.185360837448436));
#33492=CARTESIAN_POINT('Ctrl Pts',(-0.0476410511166683,0.154644758993495,
0.193313341563539));
#33493=CARTESIAN_POINT('Ctrl Pts',(-0.155840975335119,0.043569044416721,
0.201265845678642));
#33494=CARTESIAN_POINT('Ctrl Pts',(-0.120934188958227,-0.107515548465566,
0.209218349793745));
#33495=CARTESIAN_POINT('Ctrl Pts',(0.0250248668081396,-0.159870032424242,
0.217170853908847));
#33496=CARTESIAN_POINT('Ctrl Pts',(0.148003917717295,-0.0654179758516589,
0.22512335802395));
#33497=CARTESIAN_POINT('Ctrl Pts',(0.135072924616463,0.0891065444250562,
0.233075862139053));
#33498=CARTESIAN_POINT('Ctrl Pts',(-0.0018937522113587,0.161805701157652,
0.241028366254156));
#33499=CARTESIAN_POINT('Ctrl Pts',(-0.137121421381912,0.0859208183297427,
0.248980870369259));
#33500=CARTESIAN_POINT('Ctrl Pts',(-0.146432299282947,-0.0688640178244077,
0.256933374484361));
#33501=CARTESIAN_POINT('Ctrl Pts',(-0.0212763296414524,-0.160411935407873,
0.264885878599465));
#33502=CARTESIAN_POINT('Ctrl Pts',(0.123417412665197,-0.104655690124044,
0.272838382714567));
#33503=CARTESIAN_POINT('Ctrl Pts',(0.154778574015767,0.0472044939582724,
0.28079088682967));
#33504=CARTESIAN_POINT('Ctrl Pts',(0.0440086139068953,0.155717414331996,
0.288743390944773));
#33505=CARTESIAN_POINT('Ctrl Pts',(-0.107173875445849,0.121237088576372,
0.296695895059875));
#33506=CARTESIAN_POINT('Ctrl Pts',(-0.159940009655938,-0.0245736553055878,
0.304648399174979));
#33507=CARTESIAN_POINT('Ctrl Pts',(-0.0658353441931666,-0.147818735886772,
0.312600903290081));
#33508=CARTESIAN_POINT('Ctrl Pts',(0.0887250488340134,-0.135323822498093,
0.320553407405184));
#33509=CARTESIAN_POINT('Ctrl Pts',(0.161810400657075,0.00143717084316612,
0.328505911520287));
#33510=CARTESIAN_POINT('Ctrl Pts',(0.0863073974718863,0.136878429149436,
0.33645841563539));
#33511=CARTESIAN_POINT('Ctrl Pts',(-0.0684505496358049,0.146626032784815,
0.344410919750492));
#33512=CARTESIAN_POINT('Ctrl Pts',(-0.160351260416479,0.0217288858867957,
0.352363423865596));
#33513=CARTESIAN_POINT('Ctrl Pts',(-0.105003525631241,-0.123121609963769,
0.360315927980698));
#33514=CARTESIAN_POINT('Ctrl Pts',(0.0467675611965104,-0.154911156838423,
0.368268432095801));
#33515=CARTESIAN_POINT('Ctrl Pts',(0.155592612973961,-0.0444478326960028,
0.376220936210903));
#33516=CARTESIAN_POINT('Ctrl Pts',(0.121539023828006,0.106831348553276,
0.384173440326007));
#33517=CARTESIAN_POINT('Ctrl Pts',(-0.0241222499571812,0.160008714396091,
0.392125944441109));
#33518=CARTESIAN_POINT('Ctrl Pts',(-0.147632373634519,0.0662521864660413,
0.400078448556213));
#33519=CARTESIAN_POINT('Ctrl Pts',(-0.135573649464267,-0.0883428432395635,
0.408030952671315));
#33520=CARTESIAN_POINT('Ctrl Pts',(0.00098059051083778,-0.161813818534397,
0.415983456786418));
#33521=CARTESIAN_POINT('Ctrl Pts',(0.136634323339825,-0.0866932765836425,
0.423935960901521));
#33522=CARTESIAN_POINT('Ctrl Pts',(0.146818643894656,0.068036512042807,
0.431888465016623));
#33523=CARTESIAN_POINT('Ctrl Pts',(0.0221811834420201,0.160289355015634,
0.439840969131727));
#33524=CARTESIAN_POINT('Ctrl Pts',(-0.122824664094011,0.105350436989503,
0.447793473246828));
#33525=CARTESIAN_POINT('Ctrl Pts',(-0.155042815727352,-0.0463300886426471,
0.455745977361933));
#33526=CARTESIAN_POINT('Ctrl Pts',(-0.0448861093263465,-0.155466890947849,
0.463698481477034));
#33527=CARTESIAN_POINT('Ctrl Pts',(0.106486852993449,-0.121839386582653,
0.471650985592139));
#33528=CARTESIAN_POINT('Ctrl Pts',(0.160078270104732,0.0236695030909907,
0.47960348970724));
#33529=CARTESIAN_POINT('Ctrl Pts',(0.0666644623728171,0.147447020596393,
0.487555993822343));
#33530=CARTESIAN_POINT('Ctrl Pts',(-0.087952257620471,0.135818244448492,
0.495508497937446));
#33531=CARTESIAN_POINT('Ctrl Pts',(-0.161830540810569,-0.000516108099224624,
0.503461002052549));
#33532=CARTESIAN_POINT('Ctrl Pts',(-0.0870507091382164,-0.136404149983702,
0.511413506167652));
#33533=CARTESIAN_POINT('Ctrl Pts',(0.0675690001343951,-0.146981398376774,
0.519366010282755));
#33534=CARTESIAN_POINT('Ctrl Pts',(0.16032830198575,-0.0226890204033332,
0.527318514397857));
#33535=CARTESIAN_POINT('Ctrl Pts',(0.105489414021532,0.122642716620584,
0.53527101851296));
#33536=CARTESIAN_POINT('Ctrl Pts',(0.00490214493024879,0.144133374197726,
0.540572687923028));
#33537=CARTESIAN_POINT('Ctrl Pts',(-0.0388047044046456,0.131206995015769,
0.543223522628063));
#33538=CARTESIAN_POINT('Ctrl Pts',(-0.0634007094575211,0.131904027763685,
0.));
#33539=CARTESIAN_POINT('Ctrl Pts',(-0.107339749959441,0.110784382003547,
0.00265083470503427));
#33540=CARTESIAN_POINT('Ctrl Pts',(-0.171684059780304,0.0215447005535634,
0.00795250411510281));
#33541=CARTESIAN_POINT('Ctrl Pts',(-0.110860953190881,-0.133069336628884,
0.0159050082302056));
#33542=CARTESIAN_POINT('Ctrl Pts',(0.0519117226680141,-0.165059354817326,
0.0238575123453085));
#33543=CARTESIAN_POINT('Ctrl Pts',(0.166938819754359,-0.045692445844369,
0.0318100164604112));
#33544=CARTESIAN_POINT('Ctrl Pts',(0.128707834787806,0.11574507779797,0.0397625205755141));
#33545=CARTESIAN_POINT('Ctrl Pts',(-0.0277346835769849,0.170836721147544,
0.0477150246906169));
#33546=CARTESIAN_POINT('Ctrl Pts',(-0.158697852682494,0.0690821280092034,
0.0556675288057197));
#33547=CARTESIAN_POINT('Ctrl Pts',(-0.143936642246025,-0.0961259112316717,
0.0636200329208225));
#33548=CARTESIAN_POINT('Ctrl Pts',(0.00300271935518024,-0.173054250792614,
0.0715725370359253));
#33549=CARTESIAN_POINT('Ctrl Pts',(0.14718312786408,-0.0910736516165751,
0.0795250411510281));
#33550=CARTESIAN_POINT('Ctrl Pts',(0.156208052339,0.0745410449363381,0.0874775452661308));
#33551=CARTESIAN_POINT('Ctrl Pts',(0.0217887425894723,0.171704439392484,
0.0954300493812338));
#33552=CARTESIAN_POINT('Ctrl Pts',(-0.132638649479586,0.11119456839884,
0.103382553496337));
#33553=CARTESIAN_POINT('Ctrl Pts',(-0.165265842816907,-0.0514241515016591,
0.111335057611439));
#33554=CARTESIAN_POINT('Ctrl Pts',(-0.0461315298523219,-0.166820570613858,
0.119287561726542));
#33555=CARTESIAN_POINT('Ctrl Pts',(0.115364724197092,-0.129027957109734,
0.127240065841645));
#33556=CARTESIAN_POINT('Ctrl Pts',(0.170923092625556,0.0272493764316328,
0.135192569956748));
#33557=CARTESIAN_POINT('Ctrl Pts',(0.0695250318900354,0.158503940884133,
0.143145074071851));
#33558=CARTESIAN_POINT('Ctrl Pts',(-0.0957169429781459,0.144206442545789,
0.151097578186953));
#33559=CARTESIAN_POINT('Ctrl Pts',(-0.173063315155402,-0.00251393578307793,
0.159050082302056));
#33560=CARTESIAN_POINT('Ctrl Pts',(-0.0914879280754666,-0.146925796220795,
0.167002586417159));
#33561=CARTESIAN_POINT('Ctrl Pts',(0.0740996150085664,-0.156417639414764,
0.174955090532262));
#33562=CARTESIAN_POINT('Ctrl Pts',(0.171642460113959,-0.0222732279635641,
0.182907594647365));
#33563=CARTESIAN_POINT('Ctrl Pts',(0.111568299557575,0.132324394162615,
0.190860098762467));
#33564=CARTESIAN_POINT('Ctrl Pts',(-0.0509575576899273,0.165410272089882,
0.19881260287757));
#33565=CARTESIAN_POINT('Ctrl Pts',(-0.166689762399376,0.0466020803974948,
0.206765106992673));
#33566=CARTESIAN_POINT('Ctrl Pts',(-0.129352958553163,-0.115000186500534,
0.214717611107776));
#33567=CARTESIAN_POINT('Ctrl Pts',(0.0267669596738252,-0.170999300166548,
0.222670115222879));
#33568=CARTESIAN_POINT('Ctrl Pts',(0.15830713216098,-0.0699720136370574,
0.230622619337982));
#33569=CARTESIAN_POINT('Ctrl Pts',(0.144475954815417,0.0953096493813769,
0.238575123453084));
#33570=CARTESIAN_POINT('Ctrl Pts',(-0.00202558476983171,0.173069719454941,
0.246527627568187));
#33571=CARTESIAN_POINT('Ctrl Pts',(-0.146667056599619,0.091902150649062,
0.25448013168329));
#33572=CARTESIAN_POINT('Ctrl Pts',(-0.156626106340649,-0.073657949998918,
0.262432635798393));
#33573=CARTESIAN_POINT('Ctrl Pts',(-0.0227574700751082,-0.171578927439738,
0.270385139913495));
#33574=CARTESIAN_POINT('Ctrl Pts',(0.132009050564966,-0.111941240633319,
0.278337644028599));
#33575=CARTESIAN_POINT('Ctrl Pts',(0.165553402574146,0.0504906098358712,
0.286290148143701));
#33576=CARTESIAN_POINT('Ctrl Pts',(0.0470722502852127,0.16655759976238,
0.294242652258804));
#33577=CARTESIAN_POINT('Ctrl Pts',(-0.11463472809428,0.129676944368004,
0.302195156373907));
#33578=CARTESIAN_POINT('Ctrl Pts',(-0.171074148826212,-0.0262843373211962,
0.31014766048901));
#33579=CARTESIAN_POINT('Ctrl Pts',(-0.0704184368548879,-0.158109058995279,
0.318100164604112));
#33580=CARTESIAN_POINT('Ctrl Pts',(0.0949015961765597,-0.144744318820362,
0.326052668719215));
#33581=CARTESIAN_POINT('Ctrl Pts',(0.173074746107531,0.00153721873120606,
0.334005172834318));
#33582=CARTESIAN_POINT('Ctrl Pts',(0.0923156412937011,0.146407148591411,
0.341957676949421));
#33583=CARTESIAN_POINT('Ctrl Pts',(-0.0732156984410742,0.156833326497772,
0.349910181064524));
#33584=CARTESIAN_POINT('Ctrl Pts',(-0.171514028590913,0.0232415307840867,
0.357862685179626));
#33585=CARTESIAN_POINT('Ctrl Pts',(-0.112313290525359,-0.131692655714946,
0.365815189294729));
#33586=CARTESIAN_POINT('Ctrl Pts',(0.0500232602310192,-0.165695215079871,
0.373767693409832));
#33587=CARTESIAN_POINT('Ctrl Pts',(0.16642411042382,-0.0475420450579947,
0.381720197524935));
#33588=CARTESIAN_POINT('Ctrl Pts',(0.129999898682469,0.114268356373264,
0.389672701640038));
#33589=CARTESIAN_POINT('Ctrl Pts',(-0.0258015076282358,0.171147636410509,
0.39762520575514));
#33590=CARTESIAN_POINT('Ctrl Pts',(-0.157909723233413,0.0708642973820958,
0.405577709870244));
#33591=CARTESIAN_POINT('Ctrl Pts',(-0.145011537358637,-0.0944927835418238,
0.413530213985346));
#33592=CARTESIAN_POINT('Ctrl Pts',(0.00104885380055552,-0.173078401918574,
0.421482718100449));
#33593=CARTESIAN_POINT('Ctrl Pts',(0.146146049484986,-0.0927283831757074,
0.429435222215551));
#33594=CARTESIAN_POINT('Ctrl Pts',(0.157039346128141,0.0727728378400491,
0.437387726330655));
#33595=CARTESIAN_POINT('Ctrl Pts',(0.0237253147943705,0.171447813678334,
0.445340230445757));
#33596=CARTESIAN_POINT('Ctrl Pts',(-0.131375038115538,0.112684351934323,
0.45329273456086));
#33597=CARTESIAN_POINT('Ctrl Pts',(-0.16583603933271,-0.0495553332567244,
0.461245238675963));
#33598=CARTESIAN_POINT('Ctrl Pts',(-0.0480108320841284,-0.166289636325362,
0.469197742791066));
#33599=CARTESIAN_POINT('Ctrl Pts',(0.113899878937264,-0.130321171031401,
0.477150246906169));
#33600=CARTESIAN_POINT('Ctrl Pts',(0.171222034203015,0.0253172430284407,
0.485102751021271));
#33601=CARTESIAN_POINT('Ctrl Pts',(0.071305273658044,0.157711466941583,
0.493055255136374));
#33602=CARTESIAN_POINT('Ctrl Pts',(-0.0940750075114624,0.145273159693308,
0.501007759251477));
#33603=CARTESIAN_POINT('Ctrl Pts',(-0.173096288307157,-0.000552036691550711,
0.50896026336658));
#33604=CARTESIAN_POINT('Ctrl Pts',(-0.0931106982085004,-0.14589985273243,
0.516912767481683));
#33605=CARTESIAN_POINT('Ctrl Pts',(0.0722727803374284,-0.157213430677441,
0.524865271596785));
#33606=CARTESIAN_POINT('Ctrl Pts',(0.171489471921174,-0.0242685045571198,
0.532817775711888));
#33607=CARTESIAN_POINT('Ctrl Pts',(0.112833003778924,0.131180424464991,
0.540770279826991));
#33608=CARTESIAN_POINT('Ctrl Pts',(0.00524340515652838,0.154167142801661,
0.54607194923706));
#33609=CARTESIAN_POINT('Ctrl Pts',(-0.0415060733756244,0.140340900570494,
0.548722783942094));
#33610=CARTESIAN_POINT('Ctrl Pts',(-0.146267142220666,-0.000128791573925899,
0.458934495415709));
#33611=CARTESIAN_POINT('Ctrl Pts',(-0.146386413462202,-0.014310462982192,
0.459704743169127));
#33612=CARTESIAN_POINT('Ctrl Pts',(-0.144492166435918,-0.0284609503391585,
0.460474990922545));
#33613=CARTESIAN_POINT('Ctrl Pts',(-0.140455004588417,-0.04197110290299,
0.461245238675963));
#33614=CARTESIAN_POINT('Ctrl Pts',(-0.126560970249849,-0.0884667676129373,
0.463896073380997));
#33615=CARTESIAN_POINT('Ctrl Pts',(-0.0872859011669886,-0.12737820196915,
0.466546908086032));
#33616=CARTESIAN_POINT('Ctrl Pts',(-0.0406632481219932,-0.140839174931596,
0.469197742791066));
#33617=CARTESIAN_POINT('Ctrl Pts',(0.00595940492300207,-0.154300147894042,
0.4718485774961));
#33618=CARTESIAN_POINT('Ctrl Pts',(0.0599296419301325,-0.142310659462721,
0.474499412201135));
#33619=CARTESIAN_POINT('Ctrl Pts',(0.0964684529779897,-0.110376179570421,
0.477150246906169));
#33620=CARTESIAN_POINT('Ctrl Pts',(0.133007264025847,-0.0784416996781205,
0.479801081611203));
#33621=CARTESIAN_POINT('Ctrl Pts',(0.152114649114431,-0.0265622283248395,
0.482451916316237));
#33622=CARTESIAN_POINT('Ctrl Pts',(0.145015548234561,0.0214432113373248,
0.485102751021272));
#33623=CARTESIAN_POINT('Ctrl Pts',(0.137916447354691,0.0694486509994885,
0.487753585726306));
#33624=CARTESIAN_POINT('Ctrl Pts',(0.104610860506367,0.113580058970536,
0.49040442043134));
#33625=CARTESIAN_POINT('Ctrl Pts',(0.0603946868872881,0.133572711748014,
0.493055255136374));
#33626=CARTESIAN_POINT('Ctrl Pts',(0.0161785132682088,0.153565364525491,
0.495706089841409));
#33627=CARTESIAN_POINT('Ctrl Pts',(-0.0389482471216264,0.1494192621094,
0.498356924546443));
#33628=CARTESIAN_POINT('Ctrl Pts',(-0.0796818407824932,0.123042011503878,
0.501007759251477));
#33629=CARTESIAN_POINT('Ctrl Pts',(-0.0932156861533014,0.114278099486334,
0.501888506167652));
#33630=CARTESIAN_POINT('Ctrl Pts',(-0.105160643384876,0.103060050144818,
0.502769253083826));
#33631=CARTESIAN_POINT('Ctrl Pts',(-0.115072616245005,0.0902061753896192,
0.50365));
#33632=CARTESIAN_POINT('Ctrl Pts',(-0.0686153921261811,-0.0959615133978097,
-2.38524477946811E-18));
#33633=CARTESIAN_POINT('Ctrl Pts',(-0.0712073975642253,-0.0945517549303093,
-2.83889532725695E-18));
#33634=CARTESIAN_POINT('Ctrl Pts',(-0.0737377474651001,-0.0930410231931718,
5.14426139154652E-18));
#33635=CARTESIAN_POINT('Ctrl Pts',(-0.0761998018605363,-0.091430646244207,
6.50521303491303E-18));
#33636=CARTESIAN_POINT('Ctrl Pts',(-0.0821844297375259,-0.0875162295688071,
8.61254391956714E-18));
#33637=CARTESIAN_POINT('Ctrl Pts',(-0.0877662752922461,-0.0830147043174395,
8.93950144287772E-18));
#33638=CARTESIAN_POINT('Ctrl Pts',(-0.0929202787198591,-0.0780195924546499,
9.54097911787244E-18));
#33639=CARTESIAN_POINT('Ctrl Pts',(-0.0954786058604465,-0.0755401353824292,
9.83953861283751E-18));
#33640=CARTESIAN_POINT('Ctrl Pts',(-0.0979275180792717,-0.0729421130511386,
1.49939491249404E-17));
#33641=CARTESIAN_POINT('Ctrl Pts',(-0.100258897735172,-0.0702429236064683,
1.47451495458029E-17));
#33642=CARTESIAN_POINT('Ctrl Pts',(-0.104668940139426,-0.0651371314726185,
1.42745197659725E-17));
#33643=CARTESIAN_POINT('Ctrl Pts',(-0.108665118623842,-0.0596642636850333,
-1.289688799178E-17));
#33644=CARTESIAN_POINT('Ctrl Pts',(-0.112224391688578,-0.0538945629536488,
-2.42861286636753E-17));
#33645=CARTESIAN_POINT('Ctrl Pts',(-0.114007263482302,-0.0510044681210456,
-2.99911014422584E-17));
#33646=CARTESIAN_POINT('Ctrl Pts',(-0.115680198610802,-0.0480392113919056,
-9.85233076388881E-18));
#33647=CARTESIAN_POINT('Ctrl Pts',(-0.117233217251657,-0.0450208645520303,
-8.67361737988404E-18));
#33648=CARTESIAN_POINT('Ctrl Pts',(-0.121574823694362,-0.0365827983617143,
-5.37841570781424E-18));
#33649=CARTESIAN_POINT('Ctrl Pts',(-0.124997594823754,-0.027708690332575,
-9.37762199309504E-19));
#33650=CARTESIAN_POINT('Ctrl Pts',(-0.127437485841812,-0.018577962661637,
9.54097911787244E-18));
#33651=CARTESIAN_POINT('Ctrl Pts',(-0.12867484687016,-0.0139474252741679,
1.48551452162951E-17));
#33652=CARTESIAN_POINT('Ctrl Pts',(-0.129658851279119,-0.00925026145395888,
3.85592351303264E-18));
#33653=CARTESIAN_POINT('Ctrl Pts',(-0.13037677319566,-0.00450727571206391,
1.12757025938492E-17));
#33654=CARTESIAN_POINT('Ctrl Pts',(-0.130820878643177,-0.00157327166937493,
1.5865567080829E-17));
#33655=CARTESIAN_POINT('Ctrl Pts',(-0.131161668086746,0.00136911314303839,
-1.28026844144678E-17));
#33656=CARTESIAN_POINT('Ctrl Pts',(-0.131397381290232,0.00431340779322604,
-1.38777878078145E-17));
#33657=CARTESIAN_POINT('Ctrl Pts',(-0.131719489313798,0.0083368605168951,
-1.53469436465178E-17));
#33658=CARTESIAN_POINT('Ctrl Pts',(-0.131845540542961,0.0123645321806217,
2.00482317967995E-17));
#33659=CARTESIAN_POINT('Ctrl Pts',(-0.131770346471732,0.0163834363085182,
1.56125112837913E-17));
#33660=CARTESIAN_POINT('Ctrl Pts',(-0.131648667841181,0.0228868047604438,
8.25177748690449E-18));
#33661=CARTESIAN_POINT('Ctrl Pts',(-0.131000732502959,0.0293672129596454,
8.03096099599679E-18));
#33662=CARTESIAN_POINT('Ctrl Pts',(-0.129864039936534,0.0357832484813204,
1.04083408558608E-17));
#33663=CARTESIAN_POINT('Ctrl Pts',(-0.129251059617937,0.0392432020469336,
1.16903823743602E-17));
#33664=CARTESIAN_POINT('Ctrl Pts',(-0.128495732458156,0.0426844698916631,
9.6775998731851E-18));
#33665=CARTESIAN_POINT('Ctrl Pts',(-0.127602533865954,0.0461005734698996,
1.21430643318376E-17));
#33666=CARTESIAN_POINT('Ctrl Pts',(-0.126801717254801,0.0491633553806105,
1.43535300781251E-17));
#33667=CARTESIAN_POINT('Ctrl Pts',(-0.125892295195939,0.0521970927094408,
-2.04303423409802E-17));
#33668=CARTESIAN_POINT('Ctrl Pts',(-0.12487995022281,0.0551944839930744,
-1.90819582357449E-17));
#33669=CARTESIAN_POINT('Ctrl Pts',(-0.122213990144214,0.063087964688102,
-1.55310558352899E-17));
#33670=CARTESIAN_POINT('Ctrl Pts',(-0.118834573434494,0.0707355529753685,
-2.09602125306395E-19));
#33671=CARTESIAN_POINT('Ctrl Pts',(-0.114813287039476,0.0780547614149283,
-3.46944695195361E-18));
#33672=CARTESIAN_POINT('Ctrl Pts',(-0.112113271799503,0.0829691028445349,
-5.65820692756715E-18));
#33673=CARTESIAN_POINT('Ctrl Pts',(-0.109123295952561,0.0877354841888059,
1.59792597750096E-17));
#33674=CARTESIAN_POINT('Ctrl Pts',(-0.105858764968584,0.0923275350572008,
1.73472347597681E-17));
#33675=CARTESIAN_POINT('Ctrl Pts',(-0.104035851863276,0.0948917348608856,
1.81111115738308E-17));
#33676=CARTESIAN_POINT('Ctrl Pts',(-0.102127627911009,0.0974005222622627,
-1.86461934882118E-17));
#33677=CARTESIAN_POINT('Ctrl Pts',(-0.100145200306236,0.0998394990060757,
-1.56125112837913E-17));
#33678=CARTESIAN_POINT('Ctrl Pts',(-0.0936292563097381,0.10785605196023,
-5.64125013933619E-18));
#33679=CARTESIAN_POINT('Ctrl Pts',(-0.0862946795456802,0.115149852779714,
-9.28670353986392E-18));
#33680=CARTESIAN_POINT('Ctrl Pts',(-0.0782486257709069,0.121568627915854,
-1.38777878078145E-17));
#33681=CARTESIAN_POINT('Ctrl Pts',(-0.0735390572914751,0.125325707088318,
-1.65650710848099E-17));
#33682=CARTESIAN_POINT('Ctrl Pts',(-0.0685847970970084,0.128782722422648,
6.71820819248872E-19));
#33683=CARTESIAN_POINT('Ctrl Pts',(-0.0634007094575211,0.131904027763685,
0.));
#33684=CARTESIAN_POINT('Origin',(0.,0.,0.));
#33685=CARTESIAN_POINT('Origin',(-0.0577350269189626,-0.1,-0.3));
#33686=CARTESIAN_POINT('',(-0.0577350269189626,-0.1,-0.3));
#33687=CARTESIAN_POINT('',(0.0577350269189626,-0.1,-0.3));
#33688=CARTESIAN_POINT('',(-0.0288675134594813,-0.1,-0.3));
#33689=CARTESIAN_POINT('',(-0.0577350269189626,-0.1,-0.1));
#33690=CARTESIAN_POINT('',(-0.0577350269189626,-0.1,-0.3));
#33691=CARTESIAN_POINT('',(0.0577350269189626,-0.1,-0.1));
#33692=CARTESIAN_POINT('',(-0.0577350269189626,-0.1,-0.1));
#33693=CARTESIAN_POINT('',(0.0577350269189626,-0.1,-0.3));
#33694=CARTESIAN_POINT('Origin',(-0.115470053837925,1.41410031829988E-17,
-0.3));
#33695=CARTESIAN_POINT('',(-0.115470053837925,1.41410031829988E-17,-0.3));
#33696=CARTESIAN_POINT('',(-0.101036297108185,-0.025,-0.3));
#33697=CARTESIAN_POINT('',(-0.115470053837925,1.38777878078145E-17,-0.1));
#33698=CARTESIAN_POINT('',(-0.115470053837925,1.41410031829988E-17,-0.3));
#33699=CARTESIAN_POINT('',(-0.115470053837925,1.41410031829988E-17,-0.1));
#33700=CARTESIAN_POINT('Origin',(-0.0577350269189626,0.1,-0.3));
#33701=CARTESIAN_POINT('',(-0.0577350269189626,0.1,-0.3));
#33702=CARTESIAN_POINT('',(-0.0721687836487032,0.075,-0.3));
#33703=CARTESIAN_POINT('',(-0.0577350269189626,0.1,-0.1));
#33704=CARTESIAN_POINT('',(-0.0577350269189626,0.1,-0.3));
#33705=CARTESIAN_POINT('',(-0.0577350269189626,0.1,-0.1));
#33706=CARTESIAN_POINT('Origin',(0.0577350269189626,0.1,-0.3));
#33707=CARTESIAN_POINT('',(0.0577350269189626,0.1,-0.3));
#33708=CARTESIAN_POINT('',(0.0288675134594813,0.1,-0.3));
#33709=CARTESIAN_POINT('',(0.0577350269189626,0.1,-0.1));
#33710=CARTESIAN_POINT('',(0.0577350269189626,0.1,-0.3));
#33711=CARTESIAN_POINT('',(0.0577350269189626,0.1,-0.1));
#33712=CARTESIAN_POINT('Origin',(0.115470053837925,0.,-0.3));
#33713=CARTESIAN_POINT('',(0.115470053837925,0.,-0.3));
#33714=CARTESIAN_POINT('',(0.101036297108185,0.025,-0.3));
#33715=CARTESIAN_POINT('',(0.115470053837925,0.,-0.1));
#33716=CARTESIAN_POINT('',(0.115470053837925,0.,-0.3));
#33717=CARTESIAN_POINT('',(0.115470053837925,0.,-0.1));
#33718=CARTESIAN_POINT('Origin',(0.0577350269189626,-0.1,-0.3));
#33719=CARTESIAN_POINT('',(0.0721687836487032,-0.075,-0.3));
#33720=CARTESIAN_POINT('',(0.0577350269189626,-0.1,-0.1));
#33721=CARTESIAN_POINT('Origin',(0.,0.,-0.1));
#33722=CARTESIAN_POINT('Origin',(0.,0.,0.));
#33723=CARTESIAN_POINT('',(-0.3,-3.67394039744206E-17,0.));
#33724=CARTESIAN_POINT('Origin',(0.,0.,0.));
#33725=CARTESIAN_POINT('Origin',(0.,0.,-0.3));
#33726=CARTESIAN_POINT('',(-0.3,-3.67394039744206E-17,-0.3));
#33727=CARTESIAN_POINT('',(-0.3,-3.67394039744206E-17,-0.3));
#33728=CARTESIAN_POINT('Origin',(0.,0.,-0.3));
#33729=CARTESIAN_POINT('Origin',(0.,0.,-0.3));
#33730=CARTESIAN_POINT('Origin',(0.,0.,0.6));
#36461=UNCERTAINTY_MEASURE_WITH_UNIT(LENGTH_MEASURE(0.001),#36483,
'DISTANCE_ACCURACY_VALUE',
'Maximum model space distance between geometric entities at asserted c
onnectivities');
#36463=UNCERTAINTY_MEASURE_WITH_UNIT(LENGTH_MEASURE(0.001),#36483,
'DISTANCE_ACCURACY_VALUE',
'Maximum model space distance between geometric entities at asserted c
onnectivities');
#36480=(
GEOMETRIC_REPRESENTATION_CONTEXT(3)
GLOBAL_UNCERTAINTY_ASSIGNED_CONTEXT((#36461))
GLOBAL_UNIT_ASSIGNED_CONTEXT((#36483,#36485,#36486))
REPRESENTATION_CONTEXT('','3D')
);
#36482=(
GEOMETRIC_REPRESENTATION_CONTEXT(3)
GLOBAL_UNCERTAINTY_ASSIGNED_CONTEXT((#36463))
GLOBAL_UNIT_ASSIGNED_CONTEXT((#36483,#36485,#36486))
REPRESENTATION_CONTEXT('','3D')
);
#36483=(
LENGTH_UNIT()
NAMED_UNIT(*)
SI_UNIT(.CENTI.,.METRE.)
);
#36485=(
NAMED_UNIT(*)
PLANE_ANGLE_UNIT()
SI_UNIT($,.RADIAN.)
);
#36486=(
NAMED_UNIT(*)
SI_UNIT($,.STERADIAN.)
SOLID_ANGLE_UNIT()
);
#36503=SHAPE_DEFINITION_REPRESENTATION(#36521,#36570);
#36521=PRODUCT_DEFINITION_SHAPE('',$,#36589);
#36570=SHAPE_REPRESENTATION('',(#10559),#36480);
#36572=PRODUCT_DEFINITION_CONTEXT('part definition',#36628,'design');
#36589=PRODUCT_DEFINITION('Socket head cap screw M3x6',
'Socket head cap screw M3x6',#36607,#36572);
#36607=PRODUCT_DEFINITION_FORMATION('',$,#36646);
#36628=APPLICATION_CONTEXT(
'Core Data for Automotive Mechanical Design Process');
#36629=PRODUCT_CONTEXT('part definition',#36628,'mechanical');
#36646=PRODUCT('Socket head cap screw M3x6',
'Socket head cap screw M3x6',$,(#36629));
#36659=PRESENTATION_STYLE_ASSIGNMENT((#36673));
#36673=SURFACE_STYLE_USAGE(.BOTH.,#36687);
#36687=SURFACE_SIDE_STYLE('',(#36701));
#36701=SURFACE_STYLE_FILL_AREA(#36715);
#36715=FILL_AREA_STYLE('Dark gray',(#36729));
#36729=FILL_AREA_STYLE_COLOUR('Dark gray',#36743);
#36743=COLOUR_RGB('Dark gray',0.250980392156863,0.282352941176471,0.32156862745098);
ENDSEC;
END-ISO-10303-21;
